ISO-10303-21;
HEADER;
FILE_DESCRIPTION (('STEP AP203'),
    '1' );
FILE_NAME ('Spring-loaded Plate_Varsayılan.step',
    '2026-10-08T23:54:15',
    ( '' ),
    ( '' ),
    'SwSTEP 2.0',
    'SolidWorks 2024',
    '' );
FILE_SCHEMA (( 'AUTOMOTIVE_DESIGN' ));
ENDSEC;

DATA;
#14=VECTOR ( 'NONE', #49997, 1000.000000000000000 ) ;
#41=CARTESIAN_POINT ( 'NONE',  ( 8.376690734369038438, 12.50000000000004974, 2.100000000000000089 ) ) ;
#67=DIRECTION ( 'NONE',  ( 0.000000000000000000, -0.000000000000000000, -1.000000000000000000 ) ) ;
#86=VERTEX_POINT ( 'NONE', #90184 ) ;
#199=DIRECTION ( 'NONE',  ( 0.000000000000000000, 0.000000000000000000, 1.000000000000000000 ) ) ;
#200=DIRECTION ( 'NONE',  ( 0.000000000000000000, 0.000000000000000000, 1.000000000000000000 ) ) ;
#217=VECTOR ( 'NONE', #39385, 1000.000000000000000 ) ;
#224=LINE ( 'NONE', #31165, #81402 ) ;
#264=PLANE ( 'NONE',  #88586 ) ;
#297=EDGE_CURVE ( 'NONE', #11247, #80389, #48523, .T. ) ;
#338=DIRECTION ( 'NONE',  ( 0.000000000000000000, -0.000000000000000000, -1.000000000000000000 ) ) ;
#369=CARTESIAN_POINT ( 'NONE',  ( -10.34999999999999254, 2.573529411764704733, 1.544117647058823151 ) ) ;
#377=ORIENTED_EDGE ( 'NONE', *, *, #89296, .T. ) ;
#392=LINE ( 'NONE', #46576, #50078 ) ;
#394=ORIENTED_EDGE ( 'NONE', *, *, #52108, .F. ) ;
#430=ORIENTED_EDGE ( 'NONE', *, *, #35955, .T. ) ;
#449=AXIS2_PLACEMENT_3D ( 'NONE', #43723, #56962, #58459 ) ;
#454=CARTESIAN_POINT ( 'NONE',  ( 10.34999999999999254, 4.999999999999998224, 2.100000000000000089 ) ) ;
#465=CARTESIAN_POINT ( 'NONE',  ( -9.383883476483159569, 17.86611652351680846, 2.100000000000000089 ) ) ;
#472=DIRECTION ( 'NONE',  ( 1.000000000000000000, 0.000000000000000000, 0.000000000000000000 ) ) ;
#517=VECTOR ( 'NONE', #47089, 1000.000000000000000 ) ;
#529=LINE ( 'NONE', #48220, #79852 ) ;
#544=CARTESIAN_POINT ( 'NONE',  ( 2.499999999999995115, 19.99999999999999645, 2.100000000000000089 ) ) ;
#563=ORIENTED_EDGE ( 'NONE', *, *, #297, .T. ) ;
#564=LINE ( 'NONE', #70079, #40146 ) ;
#579=EDGE_CURVE ( 'NONE', #41954, #33250, #45247, .T. ) ;
#591=CARTESIAN_POINT ( 'NONE',  ( -4.621320343559618848, 12.50000000000004974, 2.100000000000000089 ) ) ;
#670=ORIENTED_EDGE ( 'NONE', *, *, #44735, .F. ) ;
#746=DIRECTION ( 'NONE',  ( -0.9848077530122087975, 0.1736481776669262789, 0.000000000000000000 ) ) ;
#760=AXIS2_PLACEMENT_3D ( 'NONE', #34476, #5513, #96870 ) ;
#764=LINE ( 'NONE', #6878, #56406 ) ;
#810=CYLINDRICAL_SURFACE ( 'NONE', #30356, 0.2499999999997798983 ) ;
#832=DIRECTION ( 'NONE',  ( 0.000000000000000000, 1.000000000000000000, -1.571307496355802709E-16 ) ) ;
#845=DIRECTION ( 'NONE',  ( 0.000000000000000000, -1.000000000000000000, 0.000000000000000000 ) ) ;
#851=( NAMED_UNIT ( * ) SI_UNIT ( $, .STERADIAN. ) SOLID_ANGLE_UNIT ( ) );
#915=VECTOR ( 'NONE', #18164, 1000.000000000000000 ) ;
#1029=LINE ( 'NONE', #92367, #64525 ) ;
#1137=ORIENTED_EDGE ( 'NONE', *, *, #28367, .F. ) ;
#1161=ORIENTED_EDGE ( 'NONE', *, *, #66445, .T. ) ;
#1165=VERTEX_POINT ( 'NONE', #9197 ) ;
#1260=AXIS2_PLACEMENT_3D ( 'NONE', #64575, #57454, #18864 ) ;
#1301=CARTESIAN_POINT ( 'NONE',  ( 10.34999999999999254, 4.999999999999998224, 2.100000000000000089 ) ) ;
#1320=FACE_OUTER_BOUND ( 'NONE', #98470, .T. ) ;
#1329=ORIENTED_EDGE ( 'NONE', *, *, #76008, .F. ) ;
#1356=CARTESIAN_POINT ( 'NONE',  ( -2.749999999999999112, 26.59999999999999432, 2.100000000000000089 ) ) ;
#1392=ORIENTED_EDGE ( 'NONE', *, *, #60505, .F. ) ;
#1411=ORIENTED_EDGE ( 'NONE', *, *, #16821, .T. ) ;
#1415=ORIENTED_EDGE ( 'NONE', *, *, #31004, .T. ) ;
#1510=EDGE_LOOP ( 'NONE', ( #95220, #92982, #52992, #14192 ) ) ;
#1533=CARTESIAN_POINT ( 'NONE',  ( 0.000000000000000000, 0.000000000000000000, 0.000000000000000000 ) ) ;
#1557=EDGE_CURVE ( 'NONE', #49884, #2918, #50780, .T. ) ;
#1566=LINE ( 'NONE', #8166, #98361 ) ;
#1580=CARTESIAN_POINT ( 'NONE',  ( 3.750000000000001332, 25.69999999999999574, 2.100000000000000089 ) ) ;
#1589=DIRECTION ( 'NONE',  ( 1.000000000000000000, 0.000000000000000000, 0.000000000000000000 ) ) ;
#1594=ORIENTED_EDGE ( 'NONE', *, *, #48663, .F. ) ;
#1788=ORIENTED_EDGE ( 'NONE', *, *, #96771, .F. ) ;
#1874=ORIENTED_EDGE ( 'NONE', *, *, #12483, .F. ) ;
#1911=ORIENTED_EDGE ( 'NONE', *, *, #36387, .F. ) ;
#1927=CARTESIAN_POINT ( 'NONE',  ( -8.499999999999987566, 18.74999999999999645, 2.100000000000000089 ) ) ;
#1951=CARTESIAN_POINT ( 'NONE',  ( -9.383883476483159569, 17.86611652351680846, 2.100000000000000089 ) ) ;
#2076=LINE ( 'NONE', #92893, #55418 ) ;
#2085=AXIS2_PLACEMENT_3D ( 'NONE', #21015, #98633, #60607 ) ;
#2128=CIRCLE ( 'NONE', #34497, 1.249999999999997558 ) ;
#2182=PLANE ( 'NONE',  #14498 ) ;
#2196=CARTESIAN_POINT ( 'NONE',  ( -8.499999999999987566, 18.74999999999999645, 2.100000000000000089 ) ) ;
#2236=CARTESIAN_POINT ( 'NONE',  ( 8.499999999999989342, 18.99999999999977973, 0.000000000000000000 ) ) ;
#2300=CARTESIAN_POINT ( 'NONE',  ( 4.621320343559255583, 11.49999999999999645, 2.100000000000000089 ) ) ;
#2314=VECTOR ( 'NONE', #20957, 1000.000000000000000 ) ;
#2443=ORIENTED_EDGE ( 'NONE', *, *, #4451, .F. ) ;
#2462=CARTESIAN_POINT ( 'NONE',  ( -1.751198251822016161, 22.56127314141087581, 0.000000000000000000 ) ) ;
#2465=CARTESIAN_POINT ( 'NONE',  ( -8.599999999999997868, 24.84999999999999787, 0.000000000000000000 ) ) ;
#2617=EDGE_CURVE ( 'NONE', #12137, #30127, #97453, .T. ) ;
#2651=ORIENTED_EDGE ( 'NONE', *, *, #8768, .F. ) ;
#2686=ORIENTED_EDGE ( 'NONE', *, *, #6352, .T. ) ;
#2693=LINE ( 'NONE', #86912, #91648 ) ;
#2699=ORIENTED_EDGE ( 'NONE', *, *, #83686, .F. ) ;
#2775=DIRECTION ( 'NONE',  ( 0.000000000000000000, 0.000000000000000000, 1.000000000000000000 ) ) ;
#2795=ORIENTED_EDGE ( 'NONE', *, *, #7638, .F. ) ;
#2813=ORIENTED_EDGE ( 'NONE', *, *, #39610, .F. ) ;
#2816=ORIENTED_EDGE ( 'NONE', *, *, #17500, .T. ) ;
#2832=ADVANCED_FACE ( 'NONE', ( #31943 ), #62913, .T. ) ;
#2859=PLANE ( 'NONE',  #64221 ) ;
#2908=EDGE_CURVE ( 'NONE', #98373, #33368, #74003, .T. ) ;
#2910=VECTOR ( 'NONE', #29364, 1000.000000000000000 ) ;
#2918=VERTEX_POINT ( 'NONE', #58286 ) ;
#2958=EDGE_CURVE ( 'NONE', #72281, #69181, #20195, .T. ) ;
#3079=DIRECTION ( 'NONE',  ( 1.000000000000000000, 0.000000000000000000, 0.000000000000000000 ) ) ;
#3150=EDGE_LOOP ( 'NONE', ( #74660, #92380, #60576, #31729 ) ) ;
#3167=EDGE_CURVE ( 'NONE', #20563, #14365, #54663, .T. ) ;
#3176=DIRECTION ( 'NONE',  ( 0.000000000000000000, -0.000000000000000000, -1.000000000000000000 ) ) ;
#3180=ORIENTED_EDGE ( 'NONE', *, *, #26797, .F. ) ;
#3219=CARTESIAN_POINT ( 'NONE',  ( -2.499999999999986677, 22.00000000000000000, 2.100000000000000089 ) ) ;
#3230=MECHANICAL_CONTEXT ( 'NONE', #80333, 'mechanical' ) ;
#3271=DIRECTION ( 'NONE',  ( 7.960204194457801640E-17, 1.000000000000000000, 0.000000000000000000 ) ) ;
#3277=VECTOR ( 'NONE', #21837, 1000.000000000000000 ) ;
#3304=ORIENTED_EDGE ( 'NONE', *, *, #297, .F. ) ;
#3367=AXIS2_PLACEMENT_3D ( 'NONE', #15901, #24517, #94031 ) ;
#3382=DIRECTION ( 'NONE',  ( 0.000000000000000000, -0.000000000000000000, -1.000000000000000000 ) ) ;
#3441=AXIS2_PLACEMENT_3D ( 'NONE', #41393, #25661, #56633 ) ;
#3523=CARTESIAN_POINT ( 'NONE',  ( 9.552245033349362461E-16, 23.99999999999999645, 2.100000000000000089 ) ) ;
#3532=DIRECTION ( 'NONE',  ( 0.000000000000000000, 1.000000000000000000, 0.000000000000000000 ) ) ;
#3535=EDGE_LOOP ( 'NONE', ( #37942, #11616, #1415, #51184 ) ) ;
#3609=FACE_OUTER_BOUND ( 'NONE', #55261, .T. ) ;
#3621=FACE_OUTER_BOUND ( 'NONE', #66225, .T. ) ;
#3643=ORIENTED_EDGE ( 'NONE', *, *, #10243, .T. ) ;
#3654=EDGE_CURVE ( 'NONE', #73030, #53704, #97055, .T. ) ;
#3662=ORIENTED_EDGE ( 'NONE', *, *, #25605, .F. ) ;
#3664=DIRECTION ( 'NONE',  ( -0.000000000000000000, -0.000000000000000000, -1.000000000000000000 ) ) ;
#3670=AXIS2_PLACEMENT_3D ( 'NONE', #39624, #8684, #72096 ) ;
#3720=DIRECTION ( 'NONE',  ( -1.000000000000000000, 0.000000000000000000, 0.000000000000000000 ) ) ;
#3769=ORIENTED_EDGE ( 'NONE', *, *, #31497, .F. ) ;
#3900=ORIENTED_EDGE ( 'NONE', *, *, #47879, .T. ) ;
#3909=ADVANCED_FACE ( 'NONE', ( #36434 ), #60790, .T. ) ;
#3963=ADVANCED_FACE ( 'NONE', ( #39439 ), #71396, .T. ) ;
#4036=AXIS2_PLACEMENT_3D ( 'NONE', #48950, #57071, #80889 ) ;
#4074=ORIENTED_EDGE ( 'NONE', *, *, #28569, .T. ) ;
#4131=VECTOR ( 'NONE', #52772, 1000.000000000000000 ) ;
#4187=DIRECTION ( 'NONE',  ( 0.000000000000000000, 0.000000000000000000, 1.000000000000000000 ) ) ;
#4244=DIRECTION ( 'NONE',  ( -1.000000000000000000, 5.782411586589363555E-16, 0.000000000000000000 ) ) ;
#4284=ADVANCED_FACE ( 'NONE', ( #7858 ), #30698, .T. ) ;
#4308=ORIENTED_EDGE ( 'NONE', *, *, #66413, .T. ) ;
#4343=DIRECTION ( 'NONE',  ( -1.000000000000000000, 7.960204194457801640E-17, 0.000000000000000000 ) ) ;
#4356=DESIGN_CONTEXT ( 'detailed design', #10995, 'design' ) ;
#4451=EDGE_CURVE ( 'NONE', #51313, #86, #13719, .T. ) ;
#4540=FACE_OUTER_BOUND ( 'NONE', #97206, .T. ) ;
#4561=CARTESIAN_POINT ( 'NONE',  ( -8.676776695296464226, 18.57322330470350735, 0.000000000000000000 ) ) ;
#4608=VECTOR ( 'NONE', #89946, 1000.000000000000000 ) ;
#4635=ORIENTED_EDGE ( 'NONE', *, *, #28569, .F. ) ;
#4657=ORIENTED_EDGE ( 'NONE', *, *, #33502, .T. ) ;
#4661=ORIENTED_EDGE ( 'NONE', *, *, #52630, .T. ) ;
#4715=AXIS2_PLACEMENT_3D ( 'NONE', #50924, #43803, #34696 ) ;
#4848=EDGE_CURVE ( 'NONE', #13991, #56450, #75558, .T. ) ;
#4855=VECTOR ( 'NONE', #55433, 1000.000000000000000 ) ;
#4861=ORIENTED_EDGE ( 'NONE', *, *, #63900, .T. ) ;
#4866=VECTOR ( 'NONE', #28348, 1000.000000000000000 ) ;
#4903=EDGE_LOOP ( 'NONE', ( #81792, #24502, #73472, #71560 ) ) ;
#4959=PLANE ( 'NONE',  #23682 ) ;
#4972=DIRECTION ( 'NONE',  ( 2.209838822900391329E-16, 1.000000000000000000, -0.000000000000000000 ) ) ;
#5036=LINE ( 'NONE', #52218, #14171 ) ;
#5058=AXIS2_PLACEMENT_3D ( 'NONE', #17680, #87697, #78559 ) ;
#5060=CARTESIAN_POINT ( 'NONE',  ( -8.599999999999997868, 24.84999999999999787, 2.100000000000000089 ) ) ;
#5121=VERTEX_POINT ( 'NONE', #22092 ) ;
#5166=EDGE_LOOP ( 'NONE', ( #2813, #43689, #51577, #67542 ) ) ;
#5243=DIRECTION ( 'NONE',  ( 0.000000000000000000, 0.000000000000000000, 1.000000000000000000 ) ) ;
#5277=CARTESIAN_POINT ( 'NONE',  ( -2.899999999999996803, 31.80000000000000071, 0.000000000000000000 ) ) ;
#5340=EDGE_CURVE ( 'NONE', #43107, #65034, #33420, .T. ) ;
#5398=LINE ( 'NONE', #26741, #23173 ) ;
#5432=VECTOR ( 'NONE', #64612, 1000.000000000000000 ) ;
#5487=CARTESIAN_POINT ( 'NONE',  ( 2.499999999999995115, 19.99999999999999645, 2.100000000000000089 ) ) ;
#5513=DIRECTION ( 'NONE',  ( -0.000000000000000000, 0.000000000000000000, 1.000000000000000000 ) ) ;
#5526=ORIENTED_EDGE ( 'NONE', *, *, #18535, .T. ) ;
#5528=CIRCLE ( 'NONE', #33129, 0.2499999999997798983 ) ;
#5541=DIRECTION ( 'NONE',  ( 0.000000000000000000, 0.000000000000000000, 1.000000000000000000 ) ) ;
#5575=CARTESIAN_POINT ( 'NONE',  ( -3.749999999999999556, 26.59999999999999432, 2.100000000000000089 ) ) ;
#5627=ORIENTED_EDGE ( 'NONE', *, *, #34312, .T. ) ;
#5755=DIRECTION ( 'NONE',  ( 0.000000000000000000, -0.000000000000000000, -1.000000000000000000 ) ) ;
#5773=DIRECTION ( 'NONE',  ( 1.000000000000000000, 0.000000000000000000, 0.000000000000000000 ) ) ;
#5782=VERTEX_POINT ( 'NONE', #55949 ) ;
#5879=ORIENTED_EDGE ( 'NONE', *, *, #48517, .F. ) ;
#5891=ORIENTED_EDGE ( 'NONE', *, *, #42071, .T. ) ;
#5892=AXIS2_PLACEMENT_3D ( 'NONE', #32686, #86971, #17463 ) ;
#5927=DIRECTION ( 'NONE',  ( -1.000000000000000000, 0.000000000000000000, 0.000000000000000000 ) ) ;
#5964=PLANE ( 'NONE',  #88970 ) ;
#6078=AXIS2_PLACEMENT_3D ( 'NONE', #58605, #13410, #73824 ) ;
#6135=AXIS2_PLACEMENT_3D ( 'NONE', #65853, #88169, #14014 ) ;
#6175=DIRECTION ( 'NONE',  ( 0.000000000000000000, -0.000000000000000000, -1.000000000000000000 ) ) ;
#6184=CARTESIAN_POINT ( 'NONE',  ( -10.34999999999999254, 0.000000000000000000, -2.500000000000001332 ) ) ;
#6203=LINE ( 'NONE', #60516, #43499 ) ;
#6225=VERTEX_POINT ( 'NONE', #22603 ) ;
#6299=ORIENTED_EDGE ( 'NONE', *, *, #7135, .F. ) ;
#6352=EDGE_CURVE ( 'NONE', #68666, #5121, #54581, .T. ) ;
#6377=ORIENTED_EDGE ( 'NONE', *, *, #29753, .F. ) ;
#6387=DIRECTION ( 'NONE',  ( -7.960204194457801640E-17, -1.000000000000000000, 0.000000000000000000 ) ) ;
#6394=AXIS2_PLACEMENT_3D ( 'NONE', #81117, #11598, #73510 ) ;
#6522=VECTOR ( 'NONE', #45204, 1000.000000000000000 ) ;
#6599=CARTESIAN_POINT ( 'NONE',  ( 4.621320343559619737, 12.50000000000004974, 2.100000000000000089 ) ) ;
#6608=ORIENTED_EDGE ( 'NONE', *, *, #46717, .F. ) ;
#6619=ORIENTED_EDGE ( 'NONE', *, *, #73743, .T. ) ;
#6648=ORIENTED_EDGE ( 'NONE', *, *, #11884, .F. ) ;
#6659=CARTESIAN_POINT ( 'NONE',  ( 8.499999999999989342, 19.99999999999999289, 2.100000000000000089 ) ) ;
#6664=LINE ( 'NONE', #12775, #23920 ) ;
#6878=CARTESIAN_POINT ( 'NONE',  ( 3.750000000000001332, 25.69999999999999574, 2.100000000000000089 ) ) ;
#6910=CIRCLE ( 'NONE', #3670, 10.80000000000000782 ) ;
#6952=CIRCLE ( 'NONE', #29689, 1.249999999999997558 ) ;
#6968=FACE_OUTER_BOUND ( 'NONE', #59418, .T. ) ;
#6981=CARTESIAN_POINT ( 'NONE',  ( -8.499999999999987566, 18.74999999999999645, 2.100000000000000089 ) ) ;
#6999=VECTOR ( 'NONE', #87776, 1000.000000000000000 ) ;
#7026=DIRECTION ( 'NONE',  ( 1.000000000000000000, 0.000000000000000000, 0.000000000000000000 ) ) ;
#7071=CARTESIAN_POINT ( 'NONE',  ( 2.750000000000001332, 27.59999999999999432, 0.000000000000000000 ) ) ;
#7135=EDGE_CURVE ( 'NONE', #66209, #98373, #22858, .T. ) ;
#7165=CARTESIAN_POINT ( 'NONE',  ( -9.299999999999991829, 12.00000000000002309, 0.000000000000000000 ) ) ;
#7258=ORIENTED_EDGE ( 'NONE', *, *, #90223, .T. ) ;
#7291=ADVANCED_FACE ( 'NONE', ( #19733 ), #96376, .T. ) ;
#7321=DIRECTION ( 'NONE',  ( -0.000000000000000000, 0.000000000000000000, 1.000000000000000000 ) ) ;
#7328=EDGE_CURVE ( 'NONE', #73980, #37074, #56838, .T. ) ;
#7338=ORIENTED_EDGE ( 'NONE', *, *, #31572, .T. ) ;
#7367=ADVANCED_FACE ( 'NONE', ( #4540 ), #66458, .F. ) ;
#7480=AXIS2_PLACEMENT_3D ( 'NONE', #8358, #56431, #31189 ) ;
#7528=ORIENTED_EDGE ( 'NONE', *, *, #96630, .F. ) ;
#7531=EDGE_CURVE ( 'NONE', #57717, #83300, #42000, .T. ) ;
#7548=LINE ( 'NONE', #1951, #63104 ) ;
#7607=EDGE_CURVE ( 'NONE', #15338, #47721, #51172, .T. ) ;
#7635=CARTESIAN_POINT ( 'NONE',  ( -10.34999999999997833, 27.69999999999999929, 0.000000000000000000 ) ) ;
#7638=EDGE_CURVE ( 'NONE', #85757, #21942, #33350, .T. ) ;
#7671=EDGE_CURVE ( 'NONE', #98207, #39922, #80352, .T. ) ;
#7672=DIRECTION ( 'NONE',  ( 1.000000000000000000, 0.000000000000000000, 0.000000000000000000 ) ) ;
#7722=LINE ( 'NONE', #92949, #13571 ) ;
#7850=CARTESIAN_POINT ( 'NONE',  ( -8.676776695296464226, 18.57322330470350735, 2.100000000000000089 ) ) ;
#7858=FACE_OUTER_BOUND ( 'NONE', #20505, .T. ) ;
#7883=LINE ( 'NONE', #29230, #32513 ) ;
#7914=ORIENTED_EDGE ( 'NONE', *, *, #96771, .T. ) ;
#7919=CARTESIAN_POINT ( 'NONE',  ( -8.499999999999987566, 18.74999999999999645, 2.100000000000000089 ) ) ;
#7930=CARTESIAN_POINT ( 'NONE',  ( 10.34999999999998010, 27.69999999999999929, 2.100000000000000089 ) ) ;
#8038=DIRECTION ( 'NONE',  ( -0.000000000000000000, -0.000000000000000000, -1.000000000000000000 ) ) ;
#8044=DIRECTION ( 'NONE',  ( 0.7071067811865513475, -0.7071067811865437980, 0.000000000000000000 ) ) ;
#8142=PLANE ( 'NONE',  #27689 ) ;
#8166=CARTESIAN_POINT ( 'NONE',  ( -10.34999999999997833, 22.00000000000000000, 0.000000000000000000 ) ) ;
#8170=MANIFOLD_SOLID_BREP ( 'Aynalama1', #37124 ) ;
#8175=AXIS2_PLACEMENT_3D ( 'NONE', #27230, #12493, #60185 ) ;
#8176=DIRECTION ( 'NONE',  ( 0.000000000000000000, 0.000000000000000000, 1.000000000000000000 ) ) ;
#8314=CARTESIAN_POINT ( 'NONE',  ( -10.34999999999999254, 12.00000000000002309, 2.100000000000000089 ) ) ;
#8358=CARTESIAN_POINT ( 'NONE',  ( 8.499999999999989342, 18.74999999999999645, 2.100000000000000089 ) ) ;
#8360=AXIS2_PLACEMENT_3D ( 'NONE', #89651, #44480, #83020 ) ;
#8379=DIRECTION ( 'NONE',  ( -0.000000000000000000, 0.000000000000000000, 1.000000000000000000 ) ) ;
#8394=DIRECTION ( 'NONE',  ( 1.000000000000000000, 0.000000000000000000, 0.000000000000000000 ) ) ;
#8400=CARTESIAN_POINT ( 'NONE',  ( 2.499999999999988454, 22.00000000000000000, 2.100000000000000089 ) ) ;
#8435=CARTESIAN_POINT ( 'NONE',  ( 8.349999999999972999, 27.69999999999999574, 2.100000000000000089 ) ) ;
#8446=LINE ( 'NONE', #46510, #66728 ) ;
#8473=EDGE_LOOP ( 'NONE', ( #59285, #51682, #15693, #51065 ) ) ;
#8588=ORIENTED_EDGE ( 'NONE', *, *, #34312, .F. ) ;
#8598=ORIENTED_EDGE ( 'NONE', *, *, #56365, .T. ) ;
#8653=EDGE_LOOP ( 'NONE', ( #1874, #64471, #30139, #33485 ) ) ;
#8658=ORIENTED_EDGE ( 'NONE', *, *, #48663, .T. ) ;
#8684=DIRECTION ( 'NONE',  ( -0.000000000000000000, -0.000000000000000000, -1.000000000000000000 ) ) ;
#8690=DIRECTION ( 'NONE',  ( -1.000000000000000000, -1.655121434032222977E-15, 0.000000000000000000 ) ) ;
#8701=EDGE_CURVE ( 'NONE', #61677, #13991, #84554, .T. ) ;
#8768=EDGE_CURVE ( 'NONE', #70766, #17712, #15142, .T. ) ;
#8803=FACE_OUTER_BOUND ( 'NONE', #19951, .T. ) ;
#8804=LINE ( 'NONE', #39243, #25312 ) ;
#8858=LINE ( 'NONE', #78853, #85200 ) ;
#8902=VERTEX_POINT ( 'NONE', #85152 ) ;
#8956=CARTESIAN_POINT ( 'NONE',  ( -6.499999999999992895, 0.000000000000000000, -2.500000000000001332 ) ) ;
#9025=AXIS2_PLACEMENT_3D ( 'NONE', #36497, #28890, #58849 ) ;
#9080=AXIS2_PLACEMENT_3D ( 'NONE', #83719, #45175, #53284 ) ;
#9175=ORIENTED_EDGE ( 'NONE', *, *, #4848, .T. ) ;
#9197=CARTESIAN_POINT ( 'NONE',  ( 9.749999999999985789, 18.74999999999999645, 0.000000000000000000 ) ) ;
#9270=ORIENTED_EDGE ( 'NONE', *, *, #13657, .T. ) ;
#9315=ADVANCED_FACE ( 'NONE', ( #70321 ), #47483, .F. ) ;
#9358=ORIENTED_EDGE ( 'NONE', *, *, #22237, .T. ) ;
#9451=CARTESIAN_POINT ( 'NONE',  ( 7.749999999999998224, 24.84999999999999787, 2.100000000000000089 ) ) ;
#9489=VERTEX_POINT ( 'NONE', #33759 ) ;
#9629=ADVANCED_FACE ( 'NONE', ( #81435 ), #90044, .T. ) ;
#9682=ORIENTED_EDGE ( 'NONE', *, *, #26797, .T. ) ;
#9689=DIRECTION ( 'NONE',  ( 0.000000000000000000, 0.000000000000000000, 1.000000000000000000 ) ) ;
#9694=EDGE_CURVE ( 'NONE', #95924, #70766, #36754, .T. ) ;
#9709=CARTESIAN_POINT ( 'NONE',  ( -2.499999999999993339, 4.999999999999997335, 0.000000000000000000 ) ) ;
#9734=EDGE_CURVE ( 'NONE', #68021, #17108, #60396, .T. ) ;
#9744=ORIENTED_EDGE ( 'NONE', *, *, #18343, .T. ) ;
#9747=LINE ( 'NONE', #79754, #4855 ) ;
#9763=AXIS2_PLACEMENT_3D ( 'NONE', #88002, #80885, #97106 ) ;
#9784=VECTOR ( 'NONE', #8038, 1000.000000000000000 ) ;
#9868=CARTESIAN_POINT ( 'NONE',  ( -4.444543648262984981, 12.92677669529668627, 2.100000000000000089 ) ) ;
#9939=DIRECTION ( 'NONE',  ( 0.000000000000000000, -1.000000000000000000, -2.891205793294678819E-16 ) ) ;
#9946=LINE ( 'NONE', #86070, #59192 ) ;
#9980=AXIS2_PLACEMENT_3D ( 'NONE', #91177, #28787, #68849 ) ;
#9987=LINE ( 'NONE', #33318, #47856 ) ;
#10145=DIRECTION ( 'NONE',  ( 0.000000000000000000, 0.000000000000000000, 1.000000000000000000 ) ) ;
#10243=EDGE_CURVE ( 'NONE', #27531, #62142, #6910, .T. ) ;
#10358=VERTEX_POINT ( 'NONE', #1580 ) ;
#10394=CARTESIAN_POINT ( 'NONE',  ( 6.499999999999992895, 1.999999999999998668, 3.499999999999999112 ) ) ;
#10406=VECTOR ( 'NONE', #82607, 1000.000000000000000 ) ;
#10543=DIRECTION ( 'NONE',  ( -1.000000000000000000, 0.000000000000000000, 0.000000000000000000 ) ) ;
#10603=AXIS2_PLACEMENT_3D ( 'NONE', #64939, #79625, #77224 ) ;
#10634=LINE ( 'NONE', #97370, #37245 ) ;
#10665=CARTESIAN_POINT ( 'NONE',  ( -10.34999999999999254, 4.999999999999999112, 0.000000000000000000 ) ) ;
#10789=VECTOR ( 'NONE', #38948, 1000.000000000000000 ) ;
#10846=ORIENTED_EDGE ( 'NONE', *, *, #64012, .T. ) ;
#10867=CARTESIAN_POINT ( 'NONE',  ( -8.349999999999971223, 27.69999999999999574, 2.100000000000000089 ) ) ;
#10937=AXIS2_PLACEMENT_3D ( 'NONE', #49505, #65248, #26150 ) ;
#10955=CARTESIAN_POINT ( 'NONE',  ( 0.000000000000000000, 0.000000000000000000, 2.100000000000000089 ) ) ;
#10995=APPLICATION_CONTEXT ( 'configuration controlled 3d designs of mechanical parts and assemblies' ) ;
#10996=ORIENTED_EDGE ( 'NONE', *, *, #73543, .T. ) ;
#11052=CARTESIAN_POINT ( 'NONE',  ( 2.750000000000001332, 26.59999999999999432, 0.000000000000000000 ) ) ;
#11130=EDGE_CURVE ( 'NONE', #91517, #6225, #54487, .T. ) ;
#11169=AXIS2_PLACEMENT_3D ( 'NONE', #3523, #12112, #43085 ) ;
#11233=CARTESIAN_POINT ( 'NONE',  ( -4.621320343559618848, 12.50000000000004974, 0.000000000000000000 ) ) ;
#11238=VECTOR ( 'NONE', #77602, 1000.000000000000000 ) ;
#11247=VERTEX_POINT ( 'NONE', #16917 ) ;
#11328=CARTESIAN_POINT ( 'NONE',  ( 2.899999999999999023, 33.29999999999999716, 2.100000000000000089 ) ) ;
#11388=ORIENTED_EDGE ( 'NONE', *, *, #7671, .F. ) ;
#11412=EDGE_CURVE ( 'NONE', #8902, #65922, #77564, .T. ) ;
#11440=CARTESIAN_POINT ( 'NONE',  ( -6.499999999999992895, 2.239999999999997105, 2.100000000000000977 ) ) ;
#11449=FACE_OUTER_BOUND ( 'NONE', #87517, .T. ) ;
#11457=DIRECTION ( 'NONE',  ( 1.000000000000000000, 0.000000000000000000, 0.000000000000000000 ) ) ;
#11598=DIRECTION ( 'NONE',  ( -0.7071067811865436870, 0.7071067811865514585, 0.000000000000000000 ) ) ;
#11616=ORIENTED_EDGE ( 'NONE', *, *, #87582, .F. ) ;
#11623=ORIENTED_EDGE ( 'NONE', *, *, #3167, .F. ) ;
#11641=VECTOR ( 'NONE', #25430, 1000.000000000000000 ) ;
#11661=PRODUCT_DEFINITION_FORMATION_WITH_SPECIFIED_SOURCE ( 'ANY', '', #71682, .NOT_KNOWN. ) ;
#11748=CARTESIAN_POINT ( 'NONE',  ( -2.899999999999996803, 31.80000000000000071, 2.100000000000000089 ) ) ;
#11759=DIRECTION ( 'NONE',  ( 1.000000000000000000, 0.000000000000000000, 0.000000000000000000 ) ) ;
#11845=ORIENTED_EDGE ( 'NONE', *, *, #17500, .F. ) ;
#11864=CYLINDRICAL_SURFACE ( 'NONE', #21055, 0.8500000000000017542 ) ;
#11867=EDGE_CURVE ( 'NONE', #98373, #68666, #61255, .T. ) ;
#11874=VECTOR ( 'NONE', #78078, 1000.000000000000000 ) ;
#11884=EDGE_CURVE ( 'NONE', #17017, #91742, #9946, .T. ) ;
#11962=VECTOR ( 'NONE', #43631, 1000.000000000000000 ) ;
#11967=EDGE_CURVE ( 'NONE', #73710, #88129, #40404, .T. ) ;
#12022=DIRECTION ( 'NONE',  ( -0.000000000000000000, -0.000000000000000000, -1.000000000000000000 ) ) ;
#12076=ORIENTED_EDGE ( 'NONE', *, *, #34893, .F. ) ;
#12097=ORIENTED_EDGE ( 'NONE', *, *, #91833, .T. ) ;
#12112=DIRECTION ( 'NONE',  ( 4.476705744456278313E-16, -1.000000000000000000, 0.000000000000000000 ) ) ;
#12118=DIRECTION ( 'NONE',  ( 0.000000000000000000, -0.5144957554275265688, 0.8574929257125440962 ) ) ;
#12137=VERTEX_POINT ( 'NONE', #34296 ) ;
#12251=AXIS2_PLACEMENT_3D ( 'NONE', #15959, #746, #77852 ) ;
#12296=DIRECTION ( 'NONE',  ( -0.000000000000000000, -0.000000000000000000, -1.000000000000000000 ) ) ;
#12319=CARTESIAN_POINT ( 'NONE',  ( 8.676776695296462449, 18.57322330470351091, 2.100000000000000089 ) ) ;
#12349=CARTESIAN_POINT ( 'NONE',  ( -2.499999999999986677, 22.00000000000000000, 2.100000000000000089 ) ) ;
#12356=CARTESIAN_POINT ( 'NONE',  ( -6.499999999999992895, 3.851859888774471706E-31, 4.499999999999999112 ) ) ;
#12412=VERTEX_POINT ( 'NONE', #11328 ) ;
#12483=EDGE_CURVE ( 'NONE', #39449, #79246, #26046, .T. ) ;
#12493=DIRECTION ( 'NONE',  ( -0.000000000000000000, -0.000000000000000000, -1.000000000000000000 ) ) ;
#12531=EDGE_CURVE ( 'NONE', #49615, #84685, #66640, .T. ) ;
#12552=ADVANCED_BREP_SHAPE_REPRESENTATION ( '', ( #8170, #37391 ), #27759 ) ;
#12579=CARTESIAN_POINT ( 'NONE',  ( 2.499999999999994671, 18.99999999999977618, 0.000000000000000000 ) ) ;
#12591=DIRECTION ( 'NONE',  ( 1.000000000000000000, -7.960204194457801640E-17, 0.000000000000000000 ) ) ;
#12624=VECTOR ( 'NONE', #59946, 1000.000000000000000 ) ;
#12675=DIRECTION ( 'NONE',  ( -0.000000000000000000, -0.000000000000000000, -1.000000000000000000 ) ) ;
#12750=PLANE ( 'NONE',  #449 ) ;
#12775=CARTESIAN_POINT ( 'NONE',  ( -8.376690734369036662, 12.50000000000004974, 2.100000000000000089 ) ) ;
#12819=AXIS2_PLACEMENT_3D ( 'NONE', #64429, #62918, #48692 ) ;
#12850=ORIENTED_EDGE ( 'NONE', *, *, #38089, .T. ) ;
#12899=LINE ( 'NONE', #29129, #89115 ) ;
#12912=DIRECTION ( 'NONE',  ( -1.000000000000000000, 0.000000000000000000, 0.000000000000000000 ) ) ;
#12954=ORIENTED_EDGE ( 'NONE', *, *, #33299, .T. ) ;
#13026=ORIENTED_EDGE ( 'NONE', *, *, #64012, .F. ) ;
#13101=EDGE_CURVE ( 'NONE', #58179, #17782, #81723, .T. ) ;
#13102=CARTESIAN_POINT ( 'NONE',  ( 4.621320343559619737, 12.50000000000004974, 2.100000000000000089 ) ) ;
#13187=PLANE ( 'NONE',  #37574 ) ;
#13198=PLANE ( 'NONE',  #36527 ) ;
#13219=EDGE_LOOP ( 'NONE', ( #26439, #89274, #9744, #26729 ) ) ;
#13250=EDGE_LOOP ( 'NONE', ( #30628, #95733, #92875, #87244 ) ) ;
#13362=ORIENTED_EDGE ( 'NONE', *, *, #31110, .F. ) ;
#13410=DIRECTION ( 'NONE',  ( 0.000000000000000000, 1.000000000000000000, 0.000000000000000000 ) ) ;
#13435=AXIS2_PLACEMENT_3D ( 'NONE', #60454, #21850, #90384 ) ;
#13568=FACE_OUTER_BOUND ( 'NONE', #29101, .T. ) ;
#13571=VECTOR ( 'NONE', #70126, 1000.000000000000000 ) ;
#13657=EDGE_CURVE ( 'NONE', #27531, #73030, #25565, .T. ) ;
#13709=EDGE_LOOP ( 'NONE', ( #8658, #43954, #7528, #95977 ) ) ;
#13719=LINE ( 'NONE', #73146, #85266 ) ;
#13722=VERTEX_POINT ( 'NONE', #73737 ) ;
#13731=LINE ( 'NONE', #7635, #6522 ) ;
#13743=CARTESIAN_POINT ( 'NONE',  ( -8.349999999999971223, 27.69999999999999574, 0.000000000000000000 ) ) ;
#13766=DIRECTION ( 'NONE',  ( -0.000000000000000000, -0.000000000000000000, -1.000000000000000000 ) ) ;
#13804=EDGE_CURVE ( 'NONE', #36030, #83300, #29550, .T. ) ;
#13900=EDGE_LOOP ( 'NONE', ( #50358, #25369, #99565, #40477 ) ) ;
#13941=DIRECTION ( 'NONE',  ( 1.000000000000000000, 0.000000000000000000, 0.000000000000000000 ) ) ;
#13947=ORIENTED_EDGE ( 'NONE', *, *, #93784, .T. ) ;
#13978=CARTESIAN_POINT ( 'NONE',  ( 2.750000000000001332, 26.59999999999999432, 2.100000000000000089 ) ) ;
#13991=VERTEX_POINT ( 'NONE', #20433 ) ;
#14014=DIRECTION ( 'NONE',  ( -1.000000000000000000, 1.734723475976801178E-15, 0.000000000000000000 ) ) ;
#14045=ADVANCED_FACE ( 'NONE', ( #61524 ), #39164, .T. ) ;
#14055=ORIENTED_EDGE ( 'NONE', *, *, #12531, .T. ) ;
#14079=CARTESIAN_POINT ( 'NONE',  ( -2.899999999999996358, 33.29999999999999716, 0.000000000000000000 ) ) ;
#14169=DIRECTION ( 'NONE',  ( -1.000000000000000000, -1.413818403454611288E-16, 0.000000000000000000 ) ) ;
#14171=VECTOR ( 'NONE', #74547, 1000.000000000000000 ) ;
#14192=ORIENTED_EDGE ( 'NONE', *, *, #71929, .T. ) ;
#14312=LINE ( 'NONE', #51904, #64022 ) ;
#14324=VECTOR ( 'NONE', #28297, 1000.000000000000000 ) ;
#14359=ORIENTED_EDGE ( 'NONE', *, *, #79148, .T. ) ;
#14365=VERTEX_POINT ( 'NONE', #76101 ) ;
#14384=ADVANCED_FACE ( 'NONE', ( #36054 ), #13198, .F. ) ;
#14389=VERTEX_POINT ( 'NONE', #52787 ) ;
#14404=ORIENTED_EDGE ( 'NONE', *, *, #77598, .T. ) ;
#14452=EDGE_LOOP ( 'NONE', ( #63582, #66439, #98198, #7338 ) ) ;
#14490=PLANE ( 'NONE',  #61442 ) ;
#14498=AXIS2_PLACEMENT_3D ( 'NONE', #16377, #70675, #16883 ) ;
#14526=ORIENTED_EDGE ( 'NONE', *, *, #84910, .F. ) ;
#14611=ORIENTED_EDGE ( 'NONE', *, *, #71060, .F. ) ;
#14663=DIRECTION ( 'NONE',  ( -0.000000000000000000, 0.000000000000000000, -1.000000000000000000 ) ) ;
#14703=CARTESIAN_POINT ( 'NONE',  ( -7.749999999999996447, 24.84999999999999787, 0.000000000000000000 ) ) ;
#14790=DIRECTION ( 'NONE',  ( 1.000000000000000000, -2.209838822900391329E-16, 0.000000000000000000 ) ) ;
#14888=ORIENTED_EDGE ( 'NONE', *, *, #27562, .T. ) ;
#14930=EDGE_CURVE ( 'NONE', #14389, #12137, #62796, .T. ) ;
#14957=LINE ( 'NONE', #7850, #30146 ) ;
#14961=EDGE_LOOP ( 'NONE', ( #51251, #53558, #88541, #40082 ) ) ;
#14992=CARTESIAN_POINT ( 'NONE',  ( 7.749999999999998224, 25.69999999999999574, 2.100000000000000089 ) ) ;
#15000=EDGE_LOOP ( 'NONE', ( #13362, #670, #22298, #35145 ) ) ;
#15049=LINE ( 'NONE', #67360, #69955 ) ;
#15088=PLANE ( 'NONE',  #67414 ) ;
#15119=ORIENTED_EDGE ( 'NONE', *, *, #56365, .F. ) ;
#15142=LINE ( 'NONE', #32372, #68418 ) ;
#15161=FACE_BOUND ( 'NONE', #27271, .T. ) ;
#15174=AXIS2_PLACEMENT_3D ( 'NONE', #99368, #29860, #7026 ) ;
#15222=VERTEX_POINT ( 'NONE', #18055 ) ;
#15265=ORIENTED_EDGE ( 'NONE', *, *, #37907, .F. ) ;
#15294=EDGE_CURVE ( 'NONE', #75526, #80526, #43406, .T. ) ;
#15295=VECTOR ( 'NONE', #55898, 1000.000000000000000 ) ;
#15338=VERTEX_POINT ( 'NONE', #29658 ) ;
#15359=DIRECTION ( 'NONE',  ( -0.000000000000000000, -0.000000000000000000, -1.000000000000000000 ) ) ;
#15489=DIRECTION ( 'NONE',  ( 5.095998543435641288E-17, 0.6401843996644797086, -0.7682212795973759611 ) ) ;
#15506=ADVANCED_FACE ( 'NONE', ( #94051 ), #70720, .T. ) ;
#15548=FACE_OUTER_BOUND ( 'NONE', #99857, .T. ) ;
#15592=AXIS2_PLACEMENT_3D ( 'NONE', #78377, #8379, #39826 ) ;
#15693=ORIENTED_EDGE ( 'NONE', *, *, #62794, .T. ) ;
#15711=FACE_OUTER_BOUND ( 'NONE', #3535, .T. ) ;
#15843=EDGE_CURVE ( 'NONE', #20587, #49615, #73119, .T. ) ;
#15883=EDGE_CURVE ( 'NONE', #91742, #89308, #42180, .T. ) ;
#15901=CARTESIAN_POINT ( 'NONE',  ( 9.299999999999993605, 12.00000000000002309, 2.100000000000000089 ) ) ;
#15917=EDGE_CURVE ( 'NONE', #17108, #49884, #5528, .T. ) ;
#15959=CARTESIAN_POINT ( 'NONE',  ( -8.349999999999971223, 27.69999999999999574, 2.100000000000000089 ) ) ;
#15969=DIRECTION ( 'NONE',  ( 1.000000000000000000, 0.000000000000000000, 0.000000000000000000 ) ) ;
#16053=DIRECTION ( 'NONE',  ( 1.000000000000000000, 0.000000000000000000, 0.000000000000000000 ) ) ;
#16072=DIRECTION ( 'NONE',  ( 1.000000000000000000, 1.413818403454611288E-16, 0.000000000000000000 ) ) ;
#16117=EDGE_LOOP ( 'NONE', ( #40731, #96901, #45217, #41573 ) ) ;
#16189=ORIENTED_EDGE ( 'NONE', *, *, #3654, .T. ) ;
#16276=CARTESIAN_POINT ( 'NONE',  ( -8.349999999999971223, 27.69999999999999574, 2.100000000000000089 ) ) ;
#16320=LINE ( 'NONE', #39656, #98799 ) ;
#16326=DIRECTION ( 'NONE',  ( -0.000000000000000000, -0.000000000000000000, -1.000000000000000000 ) ) ;
#16377=CARTESIAN_POINT ( 'NONE',  ( 8.349999999999972999, 27.69999999999999574, 2.100000000000000089 ) ) ;
#16421=DIRECTION ( 'NONE',  ( 0.000000000000000000, -1.000000000000000000, 0.000000000000000000 ) ) ;
#16461=DIRECTION ( 'NONE',  ( -0.7071067811865513475, -0.7071067811865435759, 0.000000000000000000 ) ) ;
#16482=CARTESIAN_POINT ( 'NONE',  ( -3.749999999999999556, 26.59999999999999432, 0.000000000000000000 ) ) ;
#16492=ORIENTED_EDGE ( 'NONE', *, *, #22301, .F. ) ;
#16519=VERTEX_POINT ( 'NONE', #12579 ) ;
#16612=EDGE_CURVE ( 'NONE', #12412, #97853, #68373, .T. ) ;
#16636=VERTEX_POINT ( 'NONE', #69365 ) ;
#16708=VECTOR ( 'NONE', #845, 1000.000000000000000 ) ;
#16751=ORIENTED_EDGE ( 'NONE', *, *, #23061, .T. ) ;
#16821=EDGE_CURVE ( 'NONE', #49884, #31511, #98551, .T. ) ;
#16862=DIRECTION ( 'NONE',  ( 0.000000000000000000, -0.000000000000000000, -1.000000000000000000 ) ) ;
#16879=EDGE_CURVE ( 'NONE', #85245, #79246, #14312, .T. ) ;
#16883=DIRECTION ( 'NONE',  ( 0.1736481776669261956, -0.9848077530122089085, 0.000000000000000000 ) ) ;
#16917=CARTESIAN_POINT ( 'NONE',  ( -10.34999999999999254, 4.999999999999999112, 2.100000000000000089 ) ) ;
#16969=LINE ( 'NONE', #39308, #78410 ) ;
#16974=ORIENTED_EDGE ( 'NONE', *, *, #13101, .F. ) ;
#16994=EDGE_LOOP ( 'NONE', ( #65968, #25465, #48189, #4308 ) ) ;
#17017=VERTEX_POINT ( 'NONE', #69622 ) ;
#17108=VERTEX_POINT ( 'NONE', #18821 ) ;
#17143=EDGE_CURVE ( 'NONE', #66209, #57524, #18331, .T. ) ;
#17146=EDGE_LOOP ( 'NONE', ( #6377, #50580, #75604, #91813 ) ) ;
#17193=CARTESIAN_POINT ( 'NONE',  ( -9.383883476483159569, 17.86611652351680846, 0.000000000000000000 ) ) ;
#17196=CARTESIAN_POINT ( 'NONE',  ( -8.349999999999971223, 27.69999999999999574, 2.100000000000000089 ) ) ;
#17210=DIRECTION ( 'NONE',  ( 1.000000000000000000, -5.782411586589363555E-16, 0.000000000000000000 ) ) ;
#17217=ORIENTED_EDGE ( 'NONE', *, *, #89314, .F. ) ;
#17252=PLANE ( 'NONE',  #51734 ) ;
#17259=CARTESIAN_POINT ( 'NONE',  ( 2.499999999999994671, 18.99999999999977618, 2.100000000000000089 ) ) ;
#17271=VECTOR ( 'NONE', #14790, 1000.000000000000000 ) ;
#17455=EDGE_CURVE ( 'NONE', #31222, #32160, #42925, .T. ) ;
#17463=DIRECTION ( 'NONE',  ( -1.000000000000000000, 0.000000000000000000, 0.000000000000000000 ) ) ;
#17472=CARTESIAN_POINT ( 'NONE',  ( 2.499999999999993783, 4.999999999999997335, 2.100000000000000089 ) ) ;
#17500=EDGE_CURVE ( 'NONE', #91978, #29751, #31942, .T. ) ;
#17526=ADVANCED_FACE ( 'NONE', ( #31437 ), #62912, .T. ) ;
#17568=DIRECTION ( 'NONE',  ( -0.000000000000000000, 0.000000000000000000, 1.000000000000000000 ) ) ;
#17581=DIRECTION ( 'NONE',  ( 7.960204194457801640E-17, 1.000000000000000000, 0.000000000000000000 ) ) ;
#17599=DIRECTION ( 'NONE',  ( -0.000000000000000000, 0.000000000000000000, -1.000000000000000000 ) ) ;
#17606=ORIENTED_EDGE ( 'NONE', *, *, #44984, .F. ) ;
#17616=AXIS2_PLACEMENT_3D ( 'NONE', #26689, #17568, #11457 ) ;
#17634=VECTOR ( 'NONE', #30300, 1000.000000000000000 ) ;
#17646=EDGE_CURVE ( 'NONE', #95924, #86751, #65419, .T. ) ;
#17680=CARTESIAN_POINT ( 'NONE',  ( 7.749999999999998224, 25.69999999999999574, 2.100000000000000089 ) ) ;
#17712=VERTEX_POINT ( 'NONE', #48684 ) ;
#17714=EDGE_CURVE ( 'NONE', #80254, #56196, #36597, .T. ) ;
#17782=VERTEX_POINT ( 'NONE', #50170 ) ;
#17836=VECTOR ( 'NONE', #28314, 1000.000000000000000 ) ;
#17882=EDGE_CURVE ( 'NONE', #60254, #26341, #19199, .T. ) ;
#17884=VERTEX_POINT ( 'NONE', #74002 ) ;
#17900=ORIENTED_EDGE ( 'NONE', *, *, #15294, .T. ) ;
#17982=ORIENTED_EDGE ( 'NONE', *, *, #24937, .T. ) ;
#17989=FACE_OUTER_BOUND ( 'NONE', #5166, .T. ) ;
#18009=FACE_OUTER_BOUND ( 'NONE', #71415, .T. ) ;
#18055=CARTESIAN_POINT ( 'NONE',  ( -8.499999999999987566, 19.99999999999999289, 0.000000000000000000 ) ) ;
#18164=DIRECTION ( 'NONE',  ( -0.000000000000000000, -0.000000000000000000, -1.000000000000000000 ) ) ;
#18190=VECTOR ( 'NONE', #36879, 1000.000000000000000 ) ;
#18223=PLANE ( 'NONE',  #12819 ) ;
#18252=DIRECTION ( 'NONE',  ( 4.986391167143583514E-16, -1.000000000000000000, 0.000000000000000000 ) ) ;
#18331=LINE ( 'NONE', #42194, #54296 ) ;
#18343=EDGE_CURVE ( 'NONE', #20587, #38439, #14957, .T. ) ;
#18368=CIRCLE ( 'NONE', #15174, 1.250000000000001110 ) ;
#18535=EDGE_CURVE ( 'NONE', #84685, #50583, #80427, .T. ) ;
#18680=VECTOR ( 'NONE', #29532, 1000.000000000000000 ) ;
#18691=ORIENTED_EDGE ( 'NONE', *, *, #83801, .F. ) ;
#18711=ORIENTED_EDGE ( 'NONE', *, *, #63550, .T. ) ;
#18773=CARTESIAN_POINT ( 'NONE',  ( -8.676776695296460673, 18.57322330470351091, 0.000000000000000000 ) ) ;
#18811=DIRECTION ( 'NONE',  ( 0.7071067811865515695, -0.7071067811865435759, 0.000000000000000000 ) ) ;
#18821=CARTESIAN_POINT ( 'NONE',  ( 8.749999999999769074, 18.74999999999999645, 2.100000000000000089 ) ) ;
#18851=CARTESIAN_POINT ( 'NONE',  ( -7.749999999999996447, 25.69999999999999574, 0.000000000000000000 ) ) ;
#18864=DIRECTION ( 'NONE',  ( 0.000000000000000000, 0.000000000000000000, 1.000000000000000000 ) ) ;
#18928=CIRCLE ( 'NONE', #77213, 1.050000000000000488 ) ;
#19104=ORIENTED_EDGE ( 'NONE', *, *, #28845, .T. ) ;
#19114=ORIENTED_EDGE ( 'NONE', *, *, #31662, .F. ) ;
#19199=LINE ( 'NONE', #20694, #67470 ) ;
#19204=ADVANCED_FACE ( 'NONE', ( #3621 ), #41688, .T. ) ;
#19344=CIRCLE ( 'NONE', #77644, 1.250000000000001110 ) ;
#19364=LINE ( 'NONE', #74158, #28646 ) ;
#19375=ORIENTED_EDGE ( 'NONE', *, *, #28367, .T. ) ;
#19377=ORIENTED_EDGE ( 'NONE', *, *, #45870, .F. ) ;
#19391=VERTEX_POINT ( 'NONE', #59394 ) ;
#19443=FACE_OUTER_BOUND ( 'NONE', #38362, .T. ) ;
#19572=ADVANCED_FACE ( 'NONE', ( #15711 ), #46675, .T. ) ;
#19599=CARTESIAN_POINT ( 'NONE',  ( -10.34999999999999254, 4.999999999999999112, 2.100000000000000089 ) ) ;
#19635=ORIENTED_EDGE ( 'NONE', *, *, #26671, .F. ) ;
#19733=FACE_OUTER_BOUND ( 'NONE', #33228, .T. ) ;
#19744=VECTOR ( 'NONE', #76689, 1000.000000000000000 ) ;
#19746=ORIENTED_EDGE ( 'NONE', *, *, #73543, .F. ) ;
#19784=ADVANCED_FACE ( 'NONE', ( #20198 ), #84099, .T. ) ;
#19851=DIRECTION ( 'NONE',  ( 1.000000000000000000, 0.000000000000000000, 0.000000000000000000 ) ) ;
#19885=ORIENTED_EDGE ( 'NONE', *, *, #75762, .F. ) ;
#19913=CARTESIAN_POINT ( 'NONE',  ( -9.749999999999984013, 18.74999999999999645, 2.100000000000000089 ) ) ;
#19939=CARTESIAN_POINT ( 'NONE',  ( 2.750000000000001332, 27.59999999999999432, 2.100000000000000089 ) ) ;
#19949=CIRCLE ( 'NONE', #23208, 1.250000000000001998 ) ;
#19951=EDGE_LOOP ( 'NONE', ( #96367, #9175, #19375, #11388 ) ) ;
#19957=DIRECTION ( 'NONE',  ( -1.000000000000000000, 7.960204194457801640E-17, 0.000000000000000000 ) ) ;
#20024=DIRECTION ( 'NONE',  ( 0.000000000000000000, 0.000000000000000000, -1.000000000000000000 ) ) ;
#20178=CARTESIAN_POINT ( 'NONE',  ( 2.499999999999995115, 19.99999999999999645, 2.100000000000000089 ) ) ;
#20195=LINE ( 'NONE', #43056, #38737 ) ;
#20198=FACE_OUTER_BOUND ( 'NONE', #49851, .T. ) ;
#20214=ORIENTED_EDGE ( 'NONE', *, *, #17646, .F. ) ;
#20233=ORIENTED_EDGE ( 'NONE', *, *, #52617, .F. ) ;
#20271=LINE ( 'NONE', #37010, #91339 ) ;
#20282=DIRECTION ( 'NONE',  ( 1.000000000000000000, 0.000000000000000000, 0.000000000000000000 ) ) ;
#20433=CARTESIAN_POINT ( 'NONE',  ( 10.34999999999999432, 12.00000000000002309, 2.100000000000000089 ) ) ;
#20494=DIRECTION ( 'NONE',  ( 0.000000000000000000, -0.000000000000000000, -1.000000000000000000 ) ) ;
#20505=EDGE_LOOP ( 'NONE', ( #78358, #1161, #82292, #1788 ) ) ;
#20563=VERTEX_POINT ( 'NONE', #92454 ) ;
#20587=VERTEX_POINT ( 'NONE', #32455 ) ;
#20608=CARTESIAN_POINT ( 'NONE',  ( -10.34999999999999254, 2.573529411764704733, 1.544117647058823151 ) ) ;
#20645=VECTOR ( 'NONE', #69825, 1000.000000000000000 ) ;
#20670=DIRECTION ( 'NONE',  ( -0.000000000000000000, 0.000000000000000000, -1.000000000000000000 ) ) ;
#20694=CARTESIAN_POINT ( 'NONE',  ( 6.499999999999992895, -1.784922709757266047E-15, 0.000000000000000000 ) ) ;
#20753=CARTESIAN_POINT ( 'NONE',  ( 2.499999999999997335, 4.999999999999999112, 2.100000000000000089 ) ) ;
#20882=CARTESIAN_POINT ( 'NONE',  ( 7.662324775236977636, 31.59999999999999787, 2.100000000000000089 ) ) ;
#20917=AXIS2_PLACEMENT_3D ( 'NONE', #67273, #3382, #51544 ) ;
#20921=ADVANCED_FACE ( 'NONE', ( #83619 ), #51688, .F. ) ;
#20957=DIRECTION ( 'NONE',  ( 7.960204194457801640E-17, 1.000000000000000000, 0.000000000000000000 ) ) ;
#20991=AXIS2_PLACEMENT_3D ( 'NONE', #13978, #44954, #15969 ) ;
#21006=ORIENTED_EDGE ( 'NONE', *, *, #46551, .T. ) ;
#21015=CARTESIAN_POINT ( 'NONE',  ( 8.499999999999989342, 18.74999999999999645, 2.100000000000000089 ) ) ;
#21055=AXIS2_PLACEMENT_3D ( 'NONE', #42346, #36209, #59552 ) ;
#21102=ORIENTED_EDGE ( 'NONE', *, *, #98209, .F. ) ;
#21172=EDGE_CURVE ( 'NONE', #48269, #73030, #29222, .T. ) ;
#21184=DIRECTION ( 'NONE',  ( -1.000000000000000000, 2.209838822900391329E-16, 0.000000000000000000 ) ) ;
#21398=FACE_OUTER_BOUND ( 'NONE', #52484, .T. ) ;
#21433=LINE ( 'NONE', #82844, #91367 ) ;
#21439=PLANE ( 'NONE',  #45369 ) ;
#21460=LINE ( 'NONE', #89499, #27193 ) ;
#21480=LINE ( 'NONE', #17259, #33671 ) ;
#21586=LINE ( 'NONE', #19599, #45413 ) ;
#21644=EDGE_CURVE ( 'NONE', #61677, #80660, #21460, .T. ) ;
#21810=AXIS2_PLACEMENT_3D ( 'NONE', #14703, #30933, #53787 ) ;
#21823=ADVANCED_FACE ( 'NONE', ( #39696 ), #93474, .T. ) ;
#21826=ORIENTED_EDGE ( 'NONE', *, *, #7135, .T. ) ;
#21837=DIRECTION ( 'NONE',  ( 0.000000000000000000, 0.000000000000000000, 1.000000000000000000 ) ) ;
#21850=DIRECTION ( 'NONE',  ( -0.000000000000000000, -0.000000000000000000, -1.000000000000000000 ) ) ;
#21886=VECTOR ( 'NONE', #100214, 1000.000000000000000 ) ;
#21893=ORIENTED_EDGE ( 'NONE', *, *, #13804, .F. ) ;
#21942=VERTEX_POINT ( 'NONE', #34104 ) ;
#22029=AXIS2_PLACEMENT_3D ( 'NONE', #58817, #36469, #91255 ) ;
#22048=ADVANCED_FACE ( 'NONE', ( #24971 ), #49337, .T. ) ;
#22092=CARTESIAN_POINT ( 'NONE',  ( 10.34999999999998010, 22.00000000000000000, 0.000000000000000000 ) ) ;
#22119=ORIENTED_EDGE ( 'NONE', *, *, #2958, .T. ) ;
#22131=CARTESIAN_POINT ( 'NONE',  ( 10.34999999999998010, 22.00000000000000000, 0.000000000000000000 ) ) ;
#22175=PLANE ( 'NONE',  #27401 ) ;
#22182=CARTESIAN_POINT ( 'NONE',  ( -10.34999999999999254, 1.000000000000000000, -2.500000000000001332 ) ) ;
#22216=VECTOR ( 'NONE', #70568, 1000.000000000000000 ) ;
#22237=EDGE_CURVE ( 'NONE', #56809, #15338, #35103, .T. ) ;
#22256=EDGE_CURVE ( 'NONE', #23337, #97853, #89380, .T. ) ;
#22261=LINE ( 'NONE', #69456, #88408 ) ;
#22298=ORIENTED_EDGE ( 'NONE', *, *, #98209, .T. ) ;
#22301=EDGE_CURVE ( 'NONE', #91517, #56450, #1029, .T. ) ;
#22311=CARTESIAN_POINT ( 'NONE',  ( 4.621320343559262689, 12.74999999999999645, 2.100000000000000089 ) ) ;
#22343=ORIENTED_EDGE ( 'NONE', *, *, #54568, .F. ) ;
#22391=PLANE ( 'NONE',  #5058 ) ;
#22419=DIRECTION ( 'NONE',  ( 0.000000000000000000, -1.084202172485504557E-16, 1.000000000000000000 ) ) ;
#22456=CARTESIAN_POINT ( 'NONE',  ( 1.751198251822017937, 22.56127314141087581, 2.100000000000000089 ) ) ;
#22521=CARTESIAN_POINT ( 'NONE',  ( 8.599999999999999645, 24.84999999999999787, 2.100000000000000089 ) ) ;
#22600=CARTESIAN_POINT ( 'NONE',  ( -10.34999999999999254, 0.9999999999999993339, 3.499999999999998668 ) ) ;
#22603=CARTESIAN_POINT ( 'NONE',  ( 4.621320343559255583, 11.49999999999999467, 0.000000000000000000 ) ) ;
#22620=ORIENTED_EDGE ( 'NONE', *, *, #39984, .T. ) ;
#22654=VECTOR ( 'NONE', #63721, 1000.000000000000000 ) ;
#22656=CYLINDRICAL_SURFACE ( 'NONE', #97785, 0.8500000000000017542 ) ;
#22732=EDGE_LOOP ( 'NONE', ( #39811, #39204, #1392, #89937, #67563 ) ) ;
#22820=EDGE_LOOP ( 'NONE', ( #53179, #98366, #33729, #54464 ) ) ;
#22858=LINE ( 'NONE', #544, #62538 ) ;
#22964=AXIS2_PLACEMENT_3D ( 'NONE', #74551, #98878, #52717 ) ;
#22970=DIRECTION ( 'NONE',  ( 0.000000000000000000, -0.000000000000000000, -1.000000000000000000 ) ) ;
#23061=EDGE_CURVE ( 'NONE', #74171, #73980, #34942, .T. ) ;
#23077=EDGE_CURVE ( 'NONE', #64230, #29229, #8858, .T. ) ;
#23078=ORIENTED_EDGE ( 'NONE', *, *, #30522, .F. ) ;
#23103=VECTOR ( 'NONE', #56076, 1000.000000000000000 ) ;
#23110=ORIENTED_EDGE ( 'NONE', *, *, #81738, .F. ) ;
#23138=LINE ( 'NONE', #24646, #68467 ) ;
#23173=VECTOR ( 'NONE', #82515, 1000.000000000000000 ) ;
#23191=EDGE_CURVE ( 'NONE', #13722, #68021, #95098, .T. ) ;
#23208=AXIS2_PLACEMENT_3D ( 'NONE', #35111, #3664, #96999 ) ;
#23241=ADVANCED_FACE ( 'NONE', ( #94089 ), #85476, .T. ) ;
#23252=LINE ( 'NONE', #32888, #9784 ) ;
#23263=FACE_OUTER_BOUND ( 'NONE', #1510, .T. ) ;
#23315=EDGE_LOOP ( 'NONE', ( #62346, #74772, #41162, #99251 ) ) ;
#23331=ORIENTED_EDGE ( 'NONE', *, *, #26580, .F. ) ;
#23337=VERTEX_POINT ( 'NONE', #72774 ) ;
#23375=DIRECTION ( 'NONE',  ( -1.000000000000000000, -1.655121434032222977E-15, 0.000000000000000000 ) ) ;
#23459=LINE ( 'NONE', #98604, #24808 ) ;
#23558=VERTEX_POINT ( 'NONE', #80132 ) ;
#23562=ADVANCED_FACE ( 'NONE', ( #72531 ), #62032, .T. ) ;
#23577=ORIENTED_EDGE ( 'NONE', *, *, #61355, .T. ) ;
#23682=AXIS2_PLACEMENT_3D ( 'NONE', #90689, #20670, #74466 ) ;
#23714=AXIS2_PLACEMENT_3D ( 'NONE', #26913, #12675, #97419 ) ;
#23754=LINE ( 'NONE', #94270, #14 ) ;
#23784=VECTOR ( 'NONE', #8394, 1000.000000000000000 ) ;
#23861=ORIENTED_EDGE ( 'NONE', *, *, #51614, .T. ) ;
#23879=EDGE_CURVE ( 'NONE', #21942, #33250, #92725, .T. ) ;
#23907=VECTOR ( 'NONE', #61864, 1000.000000000000000 ) ;
#23920=VECTOR ( 'NONE', #13766, 1000.000000000000000 ) ;
#23921=CARTESIAN_POINT ( 'NONE',  ( -2.499999999999986677, 22.00000000000000000, 0.000000000000000000 ) ) ;
#23998=ORIENTED_EDGE ( 'NONE', *, *, #38089, .F. ) ;
#24018=VERTEX_POINT ( 'NONE', #63315 ) ;
#24056=CARTESIAN_POINT ( 'NONE',  ( -7.749999999999996447, 25.69999999999999574, 2.100000000000000089 ) ) ;
#24057=ORIENTED_EDGE ( 'NONE', *, *, #10243, .F. ) ;
#24065=DIRECTION ( 'NONE',  ( -0.000000000000000000, -0.000000000000000000, -1.000000000000000000 ) ) ;
#24077=DIRECTION ( 'NONE',  ( 0.000000000000000000, 0.000000000000000000, 1.000000000000000000 ) ) ;
#24099=CARTESIAN_POINT ( 'NONE',  ( -2.499999999999986677, 22.00000000000000000, 0.000000000000000000 ) ) ;
#24100=CARTESIAN_POINT ( 'NONE',  ( -9.749999999999984013, 18.74999999999999645, 2.100000000000000089 ) ) ;
#24106=EDGE_LOOP ( 'NONE', ( #38093, #52276, #32211, #27998, #39686, #30836, #14359, #86830, #92115, #394, #47572, #3180 ) ) ;
#24121=LINE ( 'NONE', #8400, #22654 ) ;
#24268=EDGE_CURVE ( 'NONE', #17017, #14365, #31211, .T. ) ;
#24337=ADVANCED_FACE ( 'NONE', ( #69787 ), #264, .T. ) ;
#24380=LINE ( 'NONE', #28549, #82263 ) ;
#24498=DIRECTION ( 'NONE',  ( 0.000000000000000000, -0.000000000000000000, -1.000000000000000000 ) ) ;
#24502=ORIENTED_EDGE ( 'NONE', *, *, #74563, .T. ) ;
#24517=DIRECTION ( 'NONE',  ( 0.000000000000000000, -0.000000000000000000, -1.000000000000000000 ) ) ;
#24537=CARTESIAN_POINT ( 'NONE',  ( 9.299999999999993605, 12.00000000000002309, 2.100000000000000089 ) ) ;
#24637=PLANE ( 'NONE',  #55491 ) ;
#24646=CARTESIAN_POINT ( 'NONE',  ( -10.34999999999999254, 4.999999999999999112, 0.000000000000000000 ) ) ;
#24699=DIRECTION ( 'NONE',  ( 1.000000000000000000, 0.000000000000000000, -0.000000000000000000 ) ) ;
#24760=DIRECTION ( 'NONE',  ( -0.000000000000000000, -0.000000000000000000, -1.000000000000000000 ) ) ;
#24803=LINE ( 'NONE', #17196, #86249 ) ;
#24808=VECTOR ( 'NONE', #15359, 1000.000000000000000 ) ;
#24842=ORIENTED_EDGE ( 'NONE', *, *, #71929, .F. ) ;
#24854=DIRECTION ( 'NONE',  ( 1.000000000000000000, 0.000000000000000000, 0.000000000000000000 ) ) ;
#24861=CARTESIAN_POINT ( 'NONE',  ( 10.34999999999998010, 22.00000000000000000, 2.100000000000000089 ) ) ;
#24922=LINE ( 'NONE', #23921, #44102 ) ;
#24937=EDGE_CURVE ( 'NONE', #47723, #5782, #54607, .T. ) ;
#24971=FACE_OUTER_BOUND ( 'NONE', #42860, .T. ) ;
#24997=LINE ( 'NONE', #79285, #65412 ) ;
#25312=VECTOR ( 'NONE', #48375, 1000.000000000000000 ) ;
#25345=ORIENTED_EDGE ( 'NONE', *, *, #14930, .F. ) ;
#25359=CARTESIAN_POINT ( 'NONE',  ( 2.499999999999994671, 18.99999999999977618, 2.100000000000000089 ) ) ;
#25366=DIRECTION ( 'NONE',  ( 1.000000000000000000, 0.000000000000000000, 0.000000000000000000 ) ) ;
#25369=ORIENTED_EDGE ( 'NONE', *, *, #11967, .F. ) ;
#25376=ORIENTED_EDGE ( 'NONE', *, *, #76008, .T. ) ;
#25430=DIRECTION ( 'NONE',  ( 0.000000000000000000, 1.000000000000000000, 0.000000000000000000 ) ) ;
#25465=ORIENTED_EDGE ( 'NONE', *, *, #89296, .F. ) ;
#25467=ORIENTED_EDGE ( 'NONE', *, *, #22301, .T. ) ;
#25565=LINE ( 'NONE', #39780, #28448 ) ;
#25583=CARTESIAN_POINT ( 'NONE',  ( 2.499999999999994671, 18.99999999999977618, 2.100000000000000089 ) ) ;
#25605=EDGE_CURVE ( 'NONE', #58179, #30443, #31104, .T. ) ;
#25618=CARTESIAN_POINT ( 'NONE',  ( -2.499999999999993339, 18.99999999999977618, 2.100000000000000089 ) ) ;
#25661=DIRECTION ( 'NONE',  ( 0.000000000000000000, 0.000000000000000000, 1.000000000000000000 ) ) ;
#25683=CARTESIAN_POINT ( 'NONE',  ( 7.749999999999998224, 25.69999999999999574, 0.000000000000000000 ) ) ;
#25970=ORIENTED_EDGE ( 'NONE', *, *, #7671, .T. ) ;
#25990=AXIS2_PLACEMENT_3D ( 'NONE', #79375, #2775, #56061 ) ;
#26009=ORIENTED_EDGE ( 'NONE', *, *, #63900, .F. ) ;
#26046=LINE ( 'NONE', #95064, #47802 ) ;
#26089=CARTESIAN_POINT ( 'NONE',  ( -8.749999999999767297, 18.74999999999999645, 2.100000000000000089 ) ) ;
#26146=ORIENTED_EDGE ( 'NONE', *, *, #42404, .T. ) ;
#26150=DIRECTION ( 'NONE',  ( 1.000000000000000000, 0.000000000000000000, 0.000000000000000000 ) ) ;
#26253=EDGE_CURVE ( 'NONE', #23337, #59029, #24380, .T. ) ;
#26255=ORIENTED_EDGE ( 'NONE', *, *, #57867, .T. ) ;
#26341=VERTEX_POINT ( 'NONE', #40350 ) ;
#26384=ORIENTED_EDGE ( 'NONE', *, *, #49221, .T. ) ;
#26415=CARTESIAN_POINT ( 'NONE',  ( -10.34999999999997833, 27.69999999999999929, 0.000000000000000000 ) ) ;
#26439=ORIENTED_EDGE ( 'NONE', *, *, #66964, .F. ) ;
#26580=EDGE_CURVE ( 'NONE', #59029, #58206, #82891, .T. ) ;
#26671=EDGE_CURVE ( 'NONE', #13722, #16519, #21480, .T. ) ;
#26689=CARTESIAN_POINT ( 'NONE',  ( 4.621320343559625066, 12.75000000000004974, 2.100000000000000089 ) ) ;
#26729=ORIENTED_EDGE ( 'NONE', *, *, #73851, .F. ) ;
#26738=ORIENTED_EDGE ( 'NONE', *, *, #22256, .F. ) ;
#26741=CARTESIAN_POINT ( 'NONE',  ( 10.34999999999999254, -4.939065598916630706E-16, 2.100000000000000977 ) ) ;
#26760=ORIENTED_EDGE ( 'NONE', *, *, #24268, .T. ) ;
#26797=EDGE_CURVE ( 'NONE', #47587, #10358, #67445, .T. ) ;
#26862=EDGE_CURVE ( 'NONE', #91978, #61677, #5036, .T. ) ;
#26913=CARTESIAN_POINT ( 'NONE',  ( 7.749999999999998224, 24.84999999999999787, 2.100000000000000089 ) ) ;
#26920=DIRECTION ( 'NONE',  ( 0.000000000000000000, 0.000000000000000000, 1.000000000000000000 ) ) ;
#26936=CARTESIAN_POINT ( 'NONE',  ( 8.499999999999989342, 18.74999999999999645, 2.100000000000000089 ) ) ;
#26945=DIRECTION ( 'NONE',  ( 0.000000000000000000, 1.000000000000000000, 4.336808689942019708E-16 ) ) ;
#26995=EDGE_CURVE ( 'NONE', #16519, #87155, #31876, .T. ) ;
#27074=ORIENTED_EDGE ( 'NONE', *, *, #45870, .T. ) ;
#27193=VECTOR ( 'NONE', #5755, 1000.000000000000000 ) ;
#27201=CARTESIAN_POINT ( 'NONE',  ( 10.34999999999999254, -2.091390571243891402E-15, 0.000000000000000000 ) ) ;
#27230=CARTESIAN_POINT ( 'NONE',  ( -4.621320343559624177, 12.75000000000004974, 0.000000000000000000 ) ) ;
#27264=ADVANCED_FACE ( 'NONE', ( #40992 ), #57235, .T. ) ;
#27271=EDGE_LOOP ( 'NONE', ( #52954, #73238, #82425, #17900, #75639, #27074, #48978, #85519, #33763, #2651, #19104, #76250 ) ) ;
#27335=VECTOR ( 'NONE', #17581, 1000.000000000000000 ) ;
#27401=AXIS2_PLACEMENT_3D ( 'NONE', #66399, #4972, #21184 ) ;
#27402=DIRECTION ( 'NONE',  ( 1.000000000000000000, 0.000000000000000000, 0.000000000000000000 ) ) ;
#27415=LINE ( 'NONE', #34530, #63407 ) ;
#27507=ORIENTED_EDGE ( 'NONE', *, *, #26580, .T. ) ;
#27531=VERTEX_POINT ( 'NONE', #92639 ) ;
#27541=LINE ( 'NONE', #6184, #71495 ) ;
#27562=EDGE_CURVE ( 'NONE', #15222, #23558, #46497, .T. ) ;
#27574=CARTESIAN_POINT ( 'NONE',  ( -10.34999999999999254, 0.9999999999999997780, 1.084202172485504187E-16 ) ) ;
#27628=EDGE_CURVE ( 'NONE', #21942, #56196, #88048, .T. ) ;
#27660=PLANE ( 'NONE',  #6078 ) ;
#27689=AXIS2_PLACEMENT_3D ( 'NONE', #29965, #91364, #77128 ) ;
#27711=ORIENTED_EDGE ( 'NONE', *, *, #70987, .F. ) ;
#27759=( GEOMETRIC_REPRESENTATION_CONTEXT ( 3 ) GLOBAL_UNCERTAINTY_ASSIGNED_CONTEXT ( ( #29671 ) ) GLOBAL_UNIT_ASSIGNED_CONTEXT ( ( #46529, #53155, #851 ) ) REPRESENTATION_CONTEXT ( 'NONE', 'WORKASPACE' ) );
#27813=VERTEX_POINT ( 'NONE', #74312 ) ;
#27998=ORIENTED_EDGE ( 'NONE', *, *, #17714, .F. ) ;
#28016=CIRCLE ( 'NONE', #55545, 1.249999999999997558 ) ;
#28069=DIRECTION ( 'NONE',  ( 0.000000000000000000, 1.000000000000000000, 0.000000000000000000 ) ) ;
#28143=FACE_OUTER_BOUND ( 'NONE', #53972, .T. ) ;
#28157=DIRECTION ( 'NONE',  ( -1.000000000000000000, 0.000000000000000000, 0.000000000000000000 ) ) ;
#28295=ORIENTED_EDGE ( 'NONE', *, *, #29753, .T. ) ;
#28297=DIRECTION ( 'NONE',  ( -3.389844910009033029E-15, 1.000000000000000000, 0.000000000000000000 ) ) ;
#28314=DIRECTION ( 'NONE',  ( 1.000000000000000000, 0.000000000000000000, 0.000000000000000000 ) ) ;
#28339=CARTESIAN_POINT ( 'NONE',  ( 9.299999999999993605, 12.00000000000002309, 2.100000000000000089 ) ) ;
#28348=DIRECTION ( 'NONE',  ( 0.000000000000000000, -0.000000000000000000, -1.000000000000000000 ) ) ;
#28367=EDGE_CURVE ( 'NONE', #56450, #39922, #80186, .T. ) ;
#28419=DIRECTION ( 'NONE',  ( -1.000000000000000000, 0.000000000000000000, 0.000000000000000000 ) ) ;
#28429=DIRECTION ( 'NONE',  ( 1.000000000000000000, -0.000000000000000000, -0.000000000000000000 ) ) ;
#28434=CARTESIAN_POINT ( 'NONE',  ( -2.899999999999996803, 33.29999999999999716, 0.000000000000000000 ) ) ;
#28441=ORIENTED_EDGE ( 'NONE', *, *, #54167, .F. ) ;
#28442=CARTESIAN_POINT ( 'NONE',  ( -4.621320343559254695, 11.49999999999999467, 0.000000000000000000 ) ) ;
#28448=VECTOR ( 'NONE', #70744, 1000.000000000000000 ) ;
#28538=CARTESIAN_POINT ( 'NONE',  ( -4.621320343559254695, 11.49999999999999645, 2.100000000000000089 ) ) ;
#28549=CARTESIAN_POINT ( 'NONE',  ( -2.899999999999996803, 31.80000000000000071, 2.100000000000000089 ) ) ;
#28569=EDGE_CURVE ( 'NONE', #91742, #61087, #43128, .T. ) ;
#28646=VECTOR ( 'NONE', #50329, 1000.000000000000000 ) ;
#28671=CARTESIAN_POINT ( 'NONE',  ( -7.749999999999996447, 23.99999999999999289, 0.000000000000000000 ) ) ;
#28723=CARTESIAN_POINT ( 'NONE',  ( 3.750000000000001776, 26.59999999999999432, 2.100000000000000089 ) ) ;
#28772=FACE_OUTER_BOUND ( 'NONE', #4903, .T. ) ;
#28787=DIRECTION ( 'NONE',  ( -0.000000000000000000, -0.000000000000000000, -1.000000000000000000 ) ) ;
#28821=CARTESIAN_POINT ( 'NONE',  ( 2.499999999999995115, 19.99999999999999645, 2.100000000000000089 ) ) ;
#28828=CARTESIAN_POINT ( 'NONE',  ( 9.383883476483161346, 17.86611652351680846, 2.100000000000000089 ) ) ;
#28845=EDGE_CURVE ( 'NONE', #70766, #31222, #99989, .T. ) ;
#28890=DIRECTION ( 'NONE',  ( -1.655121434032223174E-15, 1.000000000000000000, 0.000000000000000000 ) ) ;
#28896=DIRECTION ( 'NONE',  ( 3.469446951953611033E-15, 1.000000000000000000, 0.000000000000000000 ) ) ;
#28909=LINE ( 'NONE', #89318, #86904 ) ;
#28938=CARTESIAN_POINT ( 'NONE',  ( -10.34999999999999432, 3.499999999999998668, 0.000000000000000000 ) ) ;
#28971=CARTESIAN_POINT ( 'NONE',  ( -2.499999999999993339, 19.99999999999999645, 2.100000000000000089 ) ) ;
#29068=PLANE ( 'NONE',  #64804 ) ;
#29100=ORIENTED_EDGE ( 'NONE', *, *, #49221, .F. ) ;
#29101=EDGE_LOOP ( 'NONE', ( #6608, #14611, #18711, #23861 ) ) ;
#29129=CARTESIAN_POINT ( 'NONE',  ( 6.499999999999992895, -2.035296314119462445E-15, 3.499999999999998224 ) ) ;
#29133=DIRECTION ( 'NONE',  ( -0.000000000000000000, -0.000000000000000000, -1.000000000000000000 ) ) ;
#29147=ORIENTED_EDGE ( 'NONE', *, *, #33917, .F. ) ;
#29166=ADVANCED_FACE ( 'NONE', ( #51495 ), #27660, .F. ) ;
#29181=ADVANCED_FACE ( 'NONE', ( #74326 ), #35771, .T. ) ;
#29212=ORIENTED_EDGE ( 'NONE', *, *, #86808, .T. ) ;
#29222=LINE ( 'NONE', #75885, #91925 ) ;
#29229=VERTEX_POINT ( 'NONE', #30638 ) ;
#29230=CARTESIAN_POINT ( 'NONE',  ( 6.499999999999992895, 3.983606557377048052, 3.319672131147540561 ) ) ;
#29241=CARTESIAN_POINT ( 'NONE',  ( 7.749999999999998224, 24.84999999999999787, 2.100000000000000089 ) ) ;
#29273=DIRECTION ( 'NONE',  ( 0.000000000000000000, -1.000000000000000000, 1.571307496355802463E-16 ) ) ;
#29282=DIRECTION ( 'NONE',  ( 7.960204194457801640E-17, 1.000000000000000000, 0.000000000000000000 ) ) ;
#29302=DIRECTION ( 'NONE',  ( 1.000000000000000000, -7.960204194457801640E-17, 0.000000000000000000 ) ) ;
#29324=ORIENTED_EDGE ( 'NONE', *, *, #8701, .T. ) ;
#29364=DIRECTION ( 'NONE',  ( -1.000000000000000000, 7.960204194457801640E-17, 0.000000000000000000 ) ) ;
#29522=CYLINDRICAL_SURFACE ( 'NONE', #33422, 0.8500000000000017542 ) ;
#29532=DIRECTION ( 'NONE',  ( -0.000000000000000000, -0.000000000000000000, -1.000000000000000000 ) ) ;
#29550=LINE ( 'NONE', #53407, #90037 ) ;
#29571=VECTOR ( 'NONE', #29133, 1000.000000000000000 ) ;
#29658=CARTESIAN_POINT ( 'NONE',  ( -8.499999999999987566, 19.99999999999999289, 2.100000000000000089 ) ) ;
#29661=CARTESIAN_POINT ( 'NONE',  ( -2.499999999999993339, 4.999999999999997335, 0.000000000000000000 ) ) ;
#29670=VECTOR ( 'NONE', #44915, 1000.000000000000000 ) ;
#29671=UNCERTAINTY_MEASURE_WITH_UNIT (LENGTH_MEASURE( 1.000000000000000082E-05 ), #46529, 'distance_accuracy_value', 'NONE');
#29689=AXIS2_PLACEMENT_3D ( 'NONE', #97797, #45029, #75948 ) ;
#29751=VERTEX_POINT ( 'NONE', #89812 ) ;
#29753=EDGE_CURVE ( 'NONE', #98936, #50456, #28909, .T. ) ;
#29803=CARTESIAN_POINT ( 'NONE',  ( -4.621320343559254695, 11.49999999999999645, 0.000000000000000000 ) ) ;
#29823=EDGE_LOOP ( 'NONE', ( #75131, #19746, #29212, #2816 ) ) ;
#29860=DIRECTION ( 'NONE',  ( -0.000000000000000000, 0.000000000000000000, 1.000000000000000000 ) ) ;
#29901=ORIENTED_EDGE ( 'NONE', *, *, #32641, .T. ) ;
#29950=EDGE_CURVE ( 'NONE', #89333, #62223, #83689, .T. ) ;
#29965=CARTESIAN_POINT ( 'NONE',  ( -2.499999999999993339, 4.999999999999997335, 2.100000000000000089 ) ) ;
#29978=ORIENTED_EDGE ( 'NONE', *, *, #33624, .F. ) ;
#30127=VERTEX_POINT ( 'NONE', #61700 ) ;
#30139=ORIENTED_EDGE ( 'NONE', *, *, #50080, .T. ) ;
#30142=CARTESIAN_POINT ( 'NONE',  ( -8.499999999999987566, 18.74999999999999645, 2.100000000000000089 ) ) ;
#30146=VECTOR ( 'NONE', #54046, 1000.000000000000000 ) ;
#30162=AXIS2_PLACEMENT_3D ( 'NONE', #92199, #85587, #16072 ) ;
#30199=ORIENTED_EDGE ( 'NONE', *, *, #15843, .T. ) ;
#30300=DIRECTION ( 'NONE',  ( -1.000000000000000000, 0.000000000000000000, 0.000000000000000000 ) ) ;
#30350=ORIENTED_EDGE ( 'NONE', *, *, #21644, .F. ) ;
#30356=AXIS2_PLACEMENT_3D ( 'NONE', #7919, #53616, #38867 ) ;
#30366=ADVANCED_FACE ( 'NONE', ( #28772 ), #38373, .T. ) ;
#30443=VERTEX_POINT ( 'NONE', #55619 ) ;
#30495=CIRCLE ( 'NONE', #87152, 0.8500000000000017542 ) ;
#30522=EDGE_CURVE ( 'NONE', #57524, #99197, #39090, .T. ) ;
#30550=DIRECTION ( 'NONE',  ( -1.000000000000000000, -1.413818403454611288E-16, 0.000000000000000000 ) ) ;
#30628=ORIENTED_EDGE ( 'NONE', *, *, #95726, .T. ) ;
#30629=VECTOR ( 'NONE', #30814, 1000.000000000000114 ) ;
#30638=CARTESIAN_POINT ( 'NONE',  ( -8.376690734369036662, 12.50000000000004974, 2.100000000000000089 ) ) ;
#30646=ORIENTED_EDGE ( 'NONE', *, *, #50080, .F. ) ;
#30698=CYLINDRICAL_SURFACE ( 'NONE', #7480, 1.249999999999997558 ) ;
#30701=EDGE_CURVE ( 'NONE', #69181, #73710, #63616, .T. ) ;
#30708=FACE_OUTER_BOUND ( 'NONE', #64589, .T. ) ;
#30733=LINE ( 'NONE', #53592, #88342 ) ;
#30814=DIRECTION ( 'NONE',  ( -4.095491270384932624E-17, -0.5144957554275265688, 0.8574929257125440962 ) ) ;
#30836=ORIENTED_EDGE ( 'NONE', *, *, #17646, .T. ) ;
#30892=PLANE ( 'NONE',  #83538 ) ;
#30903=DIRECTION ( 'NONE',  ( 8.630470681059372680E-33, 1.084202172485504434E-16, -1.000000000000000000 ) ) ;
#30933=DIRECTION ( 'NONE',  ( 0.000000000000000000, 0.000000000000000000, 1.000000000000000000 ) ) ;
#31004=EDGE_CURVE ( 'NONE', #90981, #58179, #72719, .T. ) ;
#31066=ORIENTED_EDGE ( 'NONE', *, *, #57867, .F. ) ;
#31104=LINE ( 'NONE', #60087, #62732 ) ;
#31109=CARTESIAN_POINT ( 'NONE',  ( 8.349999999999972999, 27.69999999999999574, 0.000000000000000000 ) ) ;
#31110=EDGE_CURVE ( 'NONE', #19391, #60254, #27541, .T. ) ;
#31135=ADVANCED_FACE ( 'NONE', ( #91918 ), #22391, .F. ) ;
#31165=CARTESIAN_POINT ( 'NONE',  ( -4.621320343559254695, 11.49999999999999467, 2.100000000000000089 ) ) ;
#31172=ORIENTED_EDGE ( 'NONE', *, *, #54568, .T. ) ;
#31189=DIRECTION ( 'NONE',  ( 1.000000000000000000, 0.000000000000000000, 0.000000000000000000 ) ) ;
#31211=LINE ( 'NONE', #46446, #80465 ) ;
#31222=VERTEX_POINT ( 'NONE', #2465 ) ;
#31277=DIRECTION ( 'NONE',  ( 0.000000000000000000, -1.571307496355802709E-16, -1.000000000000000000 ) ) ;
#31294=VECTOR ( 'NONE', #58119, 1000.000000000000114 ) ;
#31344=AXIS2_PLACEMENT_3D ( 'NONE', #53528, #7321, #13941 ) ;
#31437=FACE_OUTER_BOUND ( 'NONE', #66297, .T. ) ;
#31466=ORIENTED_EDGE ( 'NONE', *, *, #40169, .T. ) ;
#31497=EDGE_CURVE ( 'NONE', #83300, #16519, #15049, .T. ) ;
#31499=CARTESIAN_POINT ( 'NONE',  ( -2.499999999999996891, 4.999999999999999112, 2.100000000000000089 ) ) ;
#31511=VERTEX_POINT ( 'NONE', #45522 ) ;
#31564=VECTOR ( 'NONE', #46022, 1000.000000000000000 ) ;
#31572=EDGE_CURVE ( 'NONE', #87155, #16636, #71562, .T. ) ;
#31604=DIRECTION ( 'NONE',  ( -0.000000000000000000, -0.000000000000000000, -1.000000000000000000 ) ) ;
#31616=ADVANCED_FACE ( 'NONE', ( #15548 ), #56139, .F. ) ;
#31662=EDGE_CURVE ( 'NONE', #12412, #65034, #8446, .T. ) ;
#31727=ORIENTED_EDGE ( 'NONE', *, *, #75870, .T. ) ;
#31729=ORIENTED_EDGE ( 'NONE', *, *, #23879, .T. ) ;
#31730=ORIENTED_EDGE ( 'NONE', *, *, #81738, .T. ) ;
#31797=DIRECTION ( 'NONE',  ( -1.000000000000000000, 0.000000000000000000, 0.000000000000000000 ) ) ;
#31837=ORIENTED_EDGE ( 'NONE', *, *, #15883, .T. ) ;
#31876=LINE ( 'NONE', #92261, #96824 ) ;
#31942=LINE ( 'NONE', #6599, #93306 ) ;
#31943=FACE_OUTER_BOUND ( 'NONE', #8653, .T. ) ;
#32035=DIRECTION ( 'NONE',  ( 1.000000000000000000, 0.000000000000000000, 0.000000000000000000 ) ) ;
#32041=DIRECTION ( 'NONE',  ( -1.000000000000000000, 0.000000000000000000, 0.000000000000000000 ) ) ;
#32056=VERTEX_POINT ( 'NONE', #29661 ) ;
#32117=VECTOR ( 'NONE', #81721, 1000.000000000000000 ) ;
#32160=VERTEX_POINT ( 'NONE', #28671 ) ;
#32211=ORIENTED_EDGE ( 'NONE', *, *, #27628, .T. ) ;
#32271=ADVANCED_FACE ( 'NONE', ( #38766 ), #79328, .T. ) ;
#32372=CARTESIAN_POINT ( 'NONE',  ( -7.749999999999996447, 25.69999999999999574, 0.000000000000000000 ) ) ;
#32455=CARTESIAN_POINT ( 'NONE',  ( -8.676776695296464226, 18.57322330470350735, 2.100000000000000089 ) ) ;
#32486=EDGE_LOOP ( 'NONE', ( #74989, #33735, #35470, #45497 ) ) ;
#32505=DIRECTION ( 'NONE',  ( 0.000000000000000000, 1.000000000000000000, 0.000000000000000000 ) ) ;
#32513=VECTOR ( 'NONE', #15489, 1000.000000000000114 ) ;
#32633=DIRECTION ( 'NONE',  ( -0.000000000000000000, -0.000000000000000000, -1.000000000000000000 ) ) ;
#32635=LINE ( 'NONE', #33646, #80435 ) ;
#32636=EDGE_CURVE ( 'NONE', #88018, #17782, #24922, .T. ) ;
#32641=EDGE_CURVE ( 'NONE', #13991, #98207, #38646, .T. ) ;
#32682=LINE ( 'NONE', #93570, #56595 ) ;
#32686=CARTESIAN_POINT ( 'NONE',  ( -4.621320343559261801, 12.74999999999999645, 0.000000000000000000 ) ) ;
#32747=DIRECTION ( 'NONE',  ( 1.000000000000000000, 0.000000000000000000, 0.000000000000000000 ) ) ;
#32777=DIRECTION ( 'NONE',  ( 0.000000000000000000, -2.891205793294678819E-16, 1.000000000000000000 ) ) ;
#32798=ADVANCED_FACE ( 'NONE', ( #3609 ), #34054, .F. ) ;
#32802=ORIENTED_EDGE ( 'NONE', *, *, #7607, .T. ) ;
#32810=EDGE_CURVE ( 'NONE', #32056, #39449, #65030, .T. ) ;
#32827=VECTOR ( 'NONE', #55628, 1000.000000000000000 ) ;
#32888=CARTESIAN_POINT ( 'NONE',  ( -4.621320343559618848, 12.50000000000004974, 2.100000000000000089 ) ) ;
#32977=ORIENTED_EDGE ( 'NONE', *, *, #69583, .F. ) ;
#33059=ADVANCED_FACE ( 'NONE', ( #67014 ), #13187, .T. ) ;
#33097=ADVANCED_FACE ( 'NONE', ( #55279 ), #70494, .T. ) ;
#33129=AXIS2_PLACEMENT_3D ( 'NONE', #48788, #40664, #56404 ) ;
#33149=CARTESIAN_POINT ( 'NONE',  ( 7.749999999999998224, 24.84999999999999787, 0.000000000000000000 ) ) ;
#33228=EDGE_LOOP ( 'NONE', ( #60004, #83105, #43802, #69488 ) ) ;
#33244=ORIENTED_EDGE ( 'NONE', *, *, #18535, .F. ) ;
#33250=VERTEX_POINT ( 'NONE', #55783 ) ;
#33299=EDGE_CURVE ( 'NONE', #75862, #48269, #24803, .T. ) ;
#33318=CARTESIAN_POINT ( 'NONE',  ( 9.749999999999985789, 18.74999999999999645, 2.100000000000000089 ) ) ;
#33345=VECTOR ( 'NONE', #39305, 1000.000000000000000 ) ;
#33350=CIRCLE ( 'NONE', #41476, 0.8500000000000017542 ) ;
#33368=VERTEX_POINT ( 'NONE', #36303 ) ;
#33420=CIRCLE ( 'NONE', #15592, 10.80000000000000782 ) ;
#33422=AXIS2_PLACEMENT_3D ( 'NONE', #45264, #91924, #60501 ) ;
#33471=DIRECTION ( 'NONE',  ( -0.000000000000000000, -0.000000000000000000, -1.000000000000000000 ) ) ;
#33485=ORIENTED_EDGE ( 'NONE', *, *, #16879, .T. ) ;
#33492=VECTOR ( 'NONE', #63205, 1000.000000000000000 ) ;
#33502=EDGE_CURVE ( 'NONE', #36274, #50583, #224, .T. ) ;
#33556=DIRECTION ( 'NONE',  ( 0.000000000000000000, -0.000000000000000000, -1.000000000000000000 ) ) ;
#33600=ORIENTED_EDGE ( 'NONE', *, *, #83381, .T. ) ;
#33604=VERTEX_POINT ( 'NONE', #19939 ) ;
#33605=VECTOR ( 'NONE', #27402, 1000.000000000000000 ) ;
#33624=EDGE_CURVE ( 'NONE', #12137, #80389, #41291, .T. ) ;
#33638=AXIS2_PLACEMENT_3D ( 'NONE', #13102, #44068, #60806 ) ;
#33644=FACE_OUTER_BOUND ( 'NONE', #32486, .T. ) ;
#33646=CARTESIAN_POINT ( 'NONE',  ( 6.499999999999992895, -1.874386984050377894E-16, 2.100000000000000977 ) ) ;
#33654=ADVANCED_FACE ( 'NONE', ( #19443 ), #50410, .T. ) ;
#33671=VECTOR ( 'NONE', #22970, 1000.000000000000000 ) ;
#33691=AXIS2_PLACEMENT_3D ( 'NONE', #78939, #32777, #9939 ) ;
#33729=ORIENTED_EDGE ( 'NONE', *, *, #72628, .T. ) ;
#33735=ORIENTED_EDGE ( 'NONE', *, *, #66964, .T. ) ;
#33759=CARTESIAN_POINT ( 'NONE',  ( 8.349999999999972999, 27.69999999999999574, 0.000000000000000000 ) ) ;
#33763=ORIENTED_EDGE ( 'NONE', *, *, #77430, .F. ) ;
#33764=EDGE_LOOP ( 'NONE', ( #40688, #28441, #69164, #12954 ) ) ;
#33782=DIRECTION ( 'NONE',  ( -0.000000000000000000, -0.000000000000000000, -1.000000000000000000 ) ) ;
#33814=CARTESIAN_POINT ( 'NONE',  ( 2.499999999999995115, 19.99999999999999645, 0.000000000000000000 ) ) ;
#33889=LINE ( 'NONE', #64873, #44734 ) ;
#33911=DIRECTION ( 'NONE',  ( 0.000000000000000000, 1.000000000000000000, 0.000000000000000000 ) ) ;
#33917=EDGE_CURVE ( 'NONE', #65922, #60254, #70962, .T. ) ;
#33969=CARTESIAN_POINT ( 'NONE',  ( 9.383883476483161346, 17.86611652351680846, 2.100000000000000089 ) ) ;
#33979=DIRECTION ( 'NONE',  ( -1.000000000000000000, -4.986391167143583514E-16, 0.000000000000000000 ) ) ;
#34054=CYLINDRICAL_SURFACE ( 'NONE', #97542, 0.2499999999997798983 ) ;
#34099=PLANE ( 'NONE',  #38977 ) ;
#34104=CARTESIAN_POINT ( 'NONE',  ( 7.749999999999998224, 23.99999999999999289, 2.100000000000000089 ) ) ;
#34137=ORIENTED_EDGE ( 'NONE', *, *, #17143, .F. ) ;
#34271=ORIENTED_EDGE ( 'NONE', *, *, #29950, .T. ) ;
#34296=CARTESIAN_POINT ( 'NONE',  ( -10.34999999999999254, 3.499999999999996003, 0.000000000000000000 ) ) ;
#34312=EDGE_CURVE ( 'NONE', #34878, #64230, #53456, .T. ) ;
#34381=ORIENTED_EDGE ( 'NONE', *, *, #44735, .T. ) ;
#34441=CARTESIAN_POINT ( 'NONE',  ( -7.749999999999996447, 25.69999999999999574, 2.100000000000000089 ) ) ;
#34451=PLANE ( 'NONE',  #6394 ) ;
#34461=ORIENTED_EDGE ( 'NONE', *, *, #80585, .F. ) ;
#34476=CARTESIAN_POINT ( 'NONE',  ( 2.750000000000001332, 26.59999999999999432, 2.100000000000000089 ) ) ;
#34497=AXIS2_PLACEMENT_3D ( 'NONE', #30142, #200, #77308 ) ;
#34530=CARTESIAN_POINT ( 'NONE',  ( 4.444543648262985869, 12.92677669529668627, 2.100000000000000089 ) ) ;
#34532=VERTEX_POINT ( 'NONE', #28723 ) ;
#34583=DIRECTION ( 'NONE',  ( -0.7071067811865513475, -0.7071067811865435759, 0.000000000000000000 ) ) ;
#34616=EDGE_CURVE ( 'NONE', #40829, #50455, #37299, .T. ) ;
#34640=EDGE_CURVE ( 'NONE', #24018, #75990, #21586, .T. ) ;
#34647=CYLINDRICAL_SURFACE ( 'NONE', #90833, 0.2499999999997798983 ) ;
#34696=DIRECTION ( 'NONE',  ( 7.960204194457801640E-17, 1.000000000000000000, -1.571307496355802709E-16 ) ) ;
#34739=DIRECTION ( 'NONE',  ( -7.960204194457801640E-17, -1.000000000000000000, 0.000000000000000000 ) ) ;
#34816=ORIENTED_EDGE ( 'NONE', *, *, #11884, .T. ) ;
#34878=VERTEX_POINT ( 'NONE', #9868 ) ;
#34884=EDGE_CURVE ( 'NONE', #23558, #88974, #63240, .T. ) ;
#34893=EDGE_CURVE ( 'NONE', #16636, #2918, #95677, .T. ) ;
#34912=LINE ( 'NONE', #50143, #60497 ) ;
#34942=CIRCLE ( 'NONE', #52764, 1.050000000000000488 ) ;
#35005=ADVANCED_FACE ( 'NONE', ( #51437 ), #11864, .F. ) ;
#35015=CARTESIAN_POINT ( 'NONE',  ( 10.34999999999999254, 2.239999999999996216, 2.100000000000000977 ) ) ;
#35034=AXIS2_PLACEMENT_3D ( 'NONE', #72598, #72102, #49769 ) ;
#35069=DIRECTION ( 'NONE',  ( 0.000000000000000000, -1.000000000000000000, 0.000000000000000000 ) ) ;
#35103=LINE ( 'NONE', #28971, #12624 ) ;
#35111=CARTESIAN_POINT ( 'NONE',  ( -4.621320343559261801, 12.74999999999999645, 2.100000000000000089 ) ) ;
#35135=LINE ( 'NONE', #96522, #5432 ) ;
#35145=ORIENTED_EDGE ( 'NONE', *, *, #33917, .T. ) ;
#35177=LINE ( 'NONE', #66147, #65378 ) ;
#35309=AXIS2_PLACEMENT_3D ( 'NONE', #22456, #16862, #78745 ) ;
#35438=VECTOR ( 'NONE', #44771, 1000.000000000000000 ) ;
#35450=CARTESIAN_POINT ( 'NONE',  ( 6.499999999999992895, 0.9999999999999995559, -2.500000000000001332 ) ) ;
#35455=ORIENTED_EDGE ( 'NONE', *, *, #73851, .T. ) ;
#35470=ORIENTED_EDGE ( 'NONE', *, *, #88902, .F. ) ;
#35614=CARTESIAN_POINT ( 'NONE',  ( 8.499999999999989342, 18.74999999999999645, 2.100000000000000089 ) ) ;
#35731=ORIENTED_EDGE ( 'NONE', *, *, #66445, .F. ) ;
#35771=CYLINDRICAL_SURFACE ( 'NONE', #95173, 1.250000000000001998 ) ;
#35877=DIRECTION ( 'NONE',  ( 0.000000000000000000, 1.000000000000000000, 2.891205793294678326E-16 ) ) ;
#35955=EDGE_CURVE ( 'NONE', #57247, #39449, #72800, .T. ) ;
#36014=CARTESIAN_POINT ( 'NONE',  ( -10.34999999999997833, 22.00000000000000000, 2.100000000000000089 ) ) ;
#36030=VERTEX_POINT ( 'NONE', #49474 ) ;
#36054=FACE_OUTER_BOUND ( 'NONE', #36512, .T. ) ;
#36196=DIRECTION ( 'NONE',  ( 0.000000000000000000, 0.000000000000000000, -1.000000000000000000 ) ) ;
#36207=ORIENTED_EDGE ( 'NONE', *, *, #54588, .T. ) ;
#36209=DIRECTION ( 'NONE',  ( -0.000000000000000000, -0.000000000000000000, -1.000000000000000000 ) ) ;
#36274=VERTEX_POINT ( 'NONE', #87391 ) ;
#36303=CARTESIAN_POINT ( 'NONE',  ( 8.499999999999989342, 19.99999999999999289, 0.000000000000000000 ) ) ;
#36387=EDGE_CURVE ( 'NONE', #50456, #62223, #7883, .T. ) ;
#36434=FACE_OUTER_BOUND ( 'NONE', #8473, .T. ) ;
#36469=DIRECTION ( 'NONE',  ( 0.000000000000000000, -1.000000000000000000, 0.000000000000000000 ) ) ;
#36497=CARTESIAN_POINT ( 'NONE',  ( 10.34999999999998010, 27.69999999999999929, 2.100000000000000089 ) ) ;
#36512=EDGE_LOOP ( 'NONE', ( #60658, #15119, #20214, #50694 ) ) ;
#36527=AXIS2_PLACEMENT_3D ( 'NONE', #98437, #89844, #37052 ) ;
#36551=ORIENTED_EDGE ( 'NONE', *, *, #89314, .T. ) ;
#36597=CIRCLE ( 'NONE', #54494, 0.8500000000000017542 ) ;
#36617=DIRECTION ( 'NONE',  ( 0.000000000000000000, -0.000000000000000000, -1.000000000000000000 ) ) ;
#36640=EDGE_CURVE ( 'NONE', #82984, #47723, #55578, .T. ) ;
#36657=DIRECTION ( 'NONE',  ( -0.1736481776669261679, 0.9848077530122087975, 0.000000000000000000 ) ) ;
#36754=LINE ( 'NONE', #66733, #29571 ) ;
#36758=CARTESIAN_POINT ( 'NONE',  ( -2.899999999999996803, 33.29999999999999716, 2.100000000000000089 ) ) ;
#36759=AXIS2_PLACEMENT_3D ( 'NONE', #2300, #34739, #88029 ) ;
#36765=DIRECTION ( 'NONE',  ( -0.000000000000000000, -0.000000000000000000, -1.000000000000000000 ) ) ;
#36794=CARTESIAN_POINT ( 'NONE',  ( -10.34999999999997833, 27.69999999999999929, 2.100000000000000089 ) ) ;
#36879=DIRECTION ( 'NONE',  ( 0.7071067811865515695, -0.7071067811865435759, 0.000000000000000000 ) ) ;
#36896=VECTOR ( 'NONE', #3079, 1000.000000000000000 ) ;
#36928=DIRECTION ( 'NONE',  ( -7.960204194457801640E-17, -1.000000000000000000, 0.000000000000000000 ) ) ;
#37001=ADVANCED_FACE ( 'NONE', ( #81280 ), #95503, .F. ) ;
#37010=CARTESIAN_POINT ( 'NONE',  ( -2.499999999999993339, 19.99999999999999645, 0.000000000000000000 ) ) ;
#37052=DIRECTION ( 'NONE',  ( 0.000000000000000000, -0.000000000000000000, 1.000000000000000000 ) ) ;
#37074=VERTEX_POINT ( 'NONE', #97500 ) ;
#37113=ADVANCED_FACE ( 'NONE', ( #82275 ), #12750, .T. ) ;
#37124=CLOSED_SHELL ( 'NONE', ( #41482, #32798, #15506, #4284, #35005, #72990, #14045, #30366, #94782, #9629, #33654, #84405, #19204, #85392, #37113, #76372, #58368, #94444, #27264, #73499, #19572, #23562, #7367, #19784, #9315, #56964, #63321, #3909, #32271, #29181, #96836, #84196, #2832, #100211, #95521, #87357, #51717, #14384, #97446, #63787, #29166, #62383, #3963, #17526, #23241, #87832, #31616, #33059, #59003, #54024, #88952, #24337, #55071, #53702, #91477, #97019, #79669, #20921, #72916, #61133, #33097, #100031, #37001, #7291, #22048, #68369, #59539, #31135, #95583, #92890, #97435, #21823, #79926, #91857, #92963 ) ) ;
#37232=AXIS2_PLACEMENT_3D ( 'NONE', #47941, #79374, #47439 ) ;
#37245=VECTOR ( 'NONE', #12118, 1000.000000000000114 ) ;
#37299=CIRCLE ( 'NONE', #8175, 0.2500000000000011102 ) ;
#37327=VECTOR ( 'NONE', #38008, 1000.000000000000000 ) ;
#37375=VECTOR ( 'NONE', #42368, 1000.000000000000000 ) ;
#37391=AXIS2_PLACEMENT_3D ( 'NONE', #1533, #63447, #24854 ) ;
#37511=ORIENTED_EDGE ( 'NONE', *, *, #54167, .T. ) ;
#37563=CARTESIAN_POINT ( 'NONE',  ( 1.751198251822017937, 22.56127314141087581, 2.100000000000000089 ) ) ;
#37574=AXIS2_PLACEMENT_3D ( 'NONE', #97925, #28419, #59385 ) ;
#37634=DIRECTION ( 'NONE',  ( -1.000000000000000000, 0.000000000000000000, 0.000000000000000000 ) ) ;
#37832=DIRECTION ( 'NONE',  ( 0.000000000000000000, -0.000000000000000000, -1.000000000000000000 ) ) ;
#37871=CARTESIAN_POINT ( 'NONE',  ( -6.499999999999992895, -1.301042606982604926E-15, 4.499999999999999112 ) ) ;
#37877=LINE ( 'NONE', #22131, #20645 ) ;
#37907=EDGE_CURVE ( 'NONE', #93232, #26341, #92242, .T. ) ;
#37942=ORIENTED_EDGE ( 'NONE', *, *, #32636, .F. ) ;
#38008=DIRECTION ( 'NONE',  ( 0.000000000000000000, -1.000000000000000000, 1.571307496355802463E-16 ) ) ;
#38089=EDGE_CURVE ( 'NONE', #89333, #63176, #5398, .T. ) ;
#38093=ORIENTED_EDGE ( 'NONE', *, *, #55113, .T. ) ;
#38108=LINE ( 'NONE', #20882, #86202 ) ;
#38276=LINE ( 'NONE', #36794, #29670 ) ;
#38362=EDGE_LOOP ( 'NONE', ( #21102, #56609, #92260, #79016 ) ) ;
#38373=CYLINDRICAL_SURFACE ( 'NONE', #90951, 1.249999999999997558 ) ;
#38439=VERTEX_POINT ( 'NONE', #4561 ) ;
#38481=ORIENTED_EDGE ( 'NONE', *, *, #75762, .T. ) ;
#38507=DIRECTION ( 'NONE',  ( -1.000000000000000000, 0.000000000000000000, 0.000000000000000000 ) ) ;
#38535=CARTESIAN_POINT ( 'NONE',  ( 4.621320343559262689, 12.74999999999999645, 2.100000000000000089 ) ) ;
#38646=LINE ( 'NONE', #46265, #19744 ) ;
#38665=ORIENTED_EDGE ( 'NONE', *, *, #43587, .T. ) ;
#38714=CARTESIAN_POINT ( 'NONE',  ( -10.34999999999999254, 12.00000000000002309, 0.000000000000000000 ) ) ;
#38737=VECTOR ( 'NONE', #51161, 1000.000000000000000 ) ;
#38745=CIRCLE ( 'NONE', #66382, 0.2499999999997798983 ) ;
#38753=CARTESIAN_POINT ( 'NONE',  ( 10.34999999999999254, -2.091390571243891402E-15, 2.100000000000000089 ) ) ;
#38766=FACE_OUTER_BOUND ( 'NONE', #64603, .T. ) ;
#38780=EDGE_CURVE ( 'NONE', #89333, #36030, #76292, .T. ) ;
#38822=LINE ( 'NONE', #69785, #77516 ) ;
#38865=ORIENTED_EDGE ( 'NONE', *, *, #48309, .F. ) ;
#38867=DIRECTION ( 'NONE',  ( -1.000000000000000000, 0.000000000000000000, 0.000000000000000000 ) ) ;
#38914=CARTESIAN_POINT ( 'NONE',  ( 2.899999999999999467, 33.29999999999999716, 2.100000000000000089 ) ) ;
#38948=DIRECTION ( 'NONE',  ( 0.000000000000000000, -0.000000000000000000, -1.000000000000000000 ) ) ;
#38977=AXIS2_PLACEMENT_3D ( 'NONE', #48830, #79756, #65071 ) ;
#39054=DIRECTION ( 'NONE',  ( -0.000000000000000000, 0.000000000000000000, 1.000000000000000000 ) ) ;
#39060=ORIENTED_EDGE ( 'NONE', *, *, #5340, .T. ) ;
#39090=CIRCLE ( 'NONE', #66655, 1.249999999999997558 ) ;
#39164=CYLINDRICAL_SURFACE ( 'NONE', #52803, 1.050000000000000488 ) ;
#39204=ORIENTED_EDGE ( 'NONE', *, *, #7531, .F. ) ;
#39243=CARTESIAN_POINT ( 'NONE',  ( -2.749999999999999112, 27.59999999999999432, 0.000000000000000000 ) ) ;
#39258=DIRECTION ( 'NONE',  ( 0.000000000000000000, 0.000000000000000000, 1.000000000000000000 ) ) ;
#39305=DIRECTION ( 'NONE',  ( 1.000000000000000000, 4.986391167143583514E-16, 0.000000000000000000 ) ) ;
#39308=CARTESIAN_POINT ( 'NONE',  ( 9.383883476483161346, 17.86611652351680846, 2.100000000000000089 ) ) ;
#39385=DIRECTION ( 'NONE',  ( -0.000000000000000000, -0.000000000000000000, -1.000000000000000000 ) ) ;
#39397=CARTESIAN_POINT ( 'NONE',  ( 10.34999999999998010, 27.69999999999999929, 2.100000000000000089 ) ) ;
#39439=FACE_OUTER_BOUND ( 'NONE', #22820, .T. ) ;
#39449=VERTEX_POINT ( 'NONE', #58366 ) ;
#39493=CARTESIAN_POINT ( 'NONE',  ( -2.899999999999996358, 33.29999999999999716, 2.100000000000000089 ) ) ;
#39536=DIRECTION ( 'NONE',  ( -0.000000000000000000, -0.000000000000000000, -1.000000000000000000 ) ) ;
#39580=ORIENTED_EDGE ( 'NONE', *, *, #40107, .F. ) ;
#39610=EDGE_CURVE ( 'NONE', #80254, #31222, #98898, .T. ) ;
#39624=CARTESIAN_POINT ( 'NONE',  ( -1.751198251822016161, 22.56127314141087581, 2.100000000000000089 ) ) ;
#39644=CARTESIAN_POINT ( 'NONE',  ( -8.499999999999987566, 18.74999999999999645, 2.100000000000000089 ) ) ;
#39656=CARTESIAN_POINT ( 'NONE',  ( 8.599999999999999645, 24.84999999999999787, 2.100000000000000089 ) ) ;
#39662=EDGE_CURVE ( 'NONE', #82122, #88018, #20271, .T. ) ;
#39686=ORIENTED_EDGE ( 'NONE', *, *, #90892, .F. ) ;
#39696=FACE_OUTER_BOUND ( 'NONE', #42738, .T. ) ;
#39707=EDGE_CURVE ( 'NONE', #6225, #39922, #68464, .T. ) ;
#39780=CARTESIAN_POINT ( 'NONE',  ( -7.662324775236974972, 31.59999999999999787, 2.100000000000000089 ) ) ;
#39811=ORIENTED_EDGE ( 'NONE', *, *, #13804, .T. ) ;
#39826=DIRECTION ( 'NONE',  ( 1.000000000000000000, 0.000000000000000000, 0.000000000000000000 ) ) ;
#39922=VERTEX_POINT ( 'NONE', #89681 ) ;
#39984=EDGE_CURVE ( 'NONE', #11247, #14389, #84056, .T. ) ;
#40082=ORIENTED_EDGE ( 'NONE', *, *, #11967, .T. ) ;
#40107=EDGE_CURVE ( 'NONE', #80389, #32056, #23138, .T. ) ;
#40128=CARTESIAN_POINT ( 'NONE',  ( -10.34999999999997833, 22.00000000000000000, 2.100000000000000089 ) ) ;
#40146=VECTOR ( 'NONE', #67, 1000.000000000000000 ) ;
#40169=EDGE_CURVE ( 'NONE', #59693, #9489, #76926, .T. ) ;
#40202=FACE_OUTER_BOUND ( 'NONE', #13250, .T. ) ;
#40350=CARTESIAN_POINT ( 'NONE',  ( 6.499999999999992895, -5.174132726397561390E-16, 4.499999999999999112 ) ) ;
#40404=LINE ( 'NONE', #39397, #83426 ) ;
#40477=ORIENTED_EDGE ( 'NONE', *, *, #84910, .T. ) ;
#40514=DIRECTION ( 'NONE',  ( -0.000000000000000000, -0.000000000000000000, -1.000000000000000000 ) ) ;
#40529=DIRECTION ( 'NONE',  ( -1.000000000000000000, 0.000000000000000000, 0.000000000000000000 ) ) ;
#40532=DIRECTION ( 'NONE',  ( 1.000000000000000000, 0.000000000000000000, 0.000000000000000000 ) ) ;
#40576=ORIENTED_EDGE ( 'NONE', *, *, #34884, .F. ) ;
#40624=EDGE_CURVE ( 'NONE', #47721, #56484, #2128, .T. ) ;
#40664=DIRECTION ( 'NONE',  ( -0.000000000000000000, -0.000000000000000000, -1.000000000000000000 ) ) ;
#40688=ORIENTED_EDGE ( 'NONE', *, *, #93811, .F. ) ;
#40731=ORIENTED_EDGE ( 'NONE', *, *, #90892, .T. ) ;
#40762=AXIS2_PLACEMENT_3D ( 'NONE', #87069, #31277, #832 ) ;
#40821=ORIENTED_EDGE ( 'NONE', *, *, #86545, .T. ) ;
#40829=VERTEX_POINT ( 'NONE', #80713 ) ;
#40943=DIRECTION ( 'NONE',  ( 0.000000000000000000, -0.000000000000000000, -1.000000000000000000 ) ) ;
#40992=FACE_OUTER_BOUND ( 'NONE', #33764, .T. ) ;
#41058=DIRECTION ( 'NONE',  ( -5.782411586589363555E-16, -1.000000000000000000, 0.000000000000000000 ) ) ;
#41108=DIRECTION ( 'NONE',  ( -7.960204194457801640E-17, -1.000000000000000000, 0.000000000000000000 ) ) ;
#41162=ORIENTED_EDGE ( 'NONE', *, *, #62866, .T. ) ;
#41291=LINE ( 'NONE', #97569, #74524 ) ;
#41325=PLANE ( 'NONE',  #37232 ) ;
#41393=CARTESIAN_POINT ( 'NONE',  ( -8.499999999999987566, 18.74999999999999645, 0.000000000000000000 ) ) ;
#41420=ORIENTED_EDGE ( 'NONE', *, *, #79148, .F. ) ;
#41476=AXIS2_PLACEMENT_3D ( 'NONE', #29241, #12022, #42991 ) ;
#41482=ADVANCED_FACE ( 'NONE', ( #84570 ), #22656, .F. ) ;
#41573=ORIENTED_EDGE ( 'NONE', *, *, #9694, .F. ) ;
#41612=CARTESIAN_POINT ( 'NONE',  ( 2.750000000000001332, 27.59999999999999432, 2.100000000000000089 ) ) ;
#41661=PLANE ( 'NONE',  #78735 ) ;
#41688=PLANE ( 'NONE',  #85331 ) ;
#41881=DIRECTION ( 'NONE',  ( 0.000000000000000000, 0.000000000000000000, 1.000000000000000000 ) ) ;
#41954=VERTEX_POINT ( 'NONE', #80340 ) ;
#41983=ORIENTED_EDGE ( 'NONE', *, *, #33299, .F. ) ;
#42000=LINE ( 'NONE', #64852, #98163 ) ;
#42071=EDGE_CURVE ( 'NONE', #57281, #5782, #35177, .T. ) ;
#42180=LINE ( 'NONE', #47776, #15295 ) ;
#42190=VECTOR ( 'NONE', #5541, 1000.000000000000000 ) ;
#42194=CARTESIAN_POINT ( 'NONE',  ( 2.499999999999995115, 19.99999999999999645, 2.100000000000000089 ) ) ;
#42223=ORIENTED_EDGE ( 'NONE', *, *, #73199, .F. ) ;
#42299=LINE ( 'NONE', #73228, #61376 ) ;
#42327=PLANE ( 'NONE',  #4715 ) ;
#42346=CARTESIAN_POINT ( 'NONE',  ( -7.749999999999996447, 24.84999999999999787, 2.100000000000000089 ) ) ;
#42368=DIRECTION ( 'NONE',  ( -0.000000000000000000, -0.000000000000000000, -1.000000000000000000 ) ) ;
#42400=LINE ( 'NONE', #73334, #31294 ) ;
#42404=EDGE_CURVE ( 'NONE', #98936, #24018, #42400, .T. ) ;
#42440=LINE ( 'NONE', #27201, #27335 ) ;
#42465=ORIENTED_EDGE ( 'NONE', *, *, #12483, .T. ) ;
#42516=DIRECTION ( 'NONE',  ( 1.000000000000000000, 0.000000000000000000, 0.000000000000000000 ) ) ;
#42553=VECTOR ( 'NONE', #90297, 1000.000000000000000 ) ;
#42695=VECTOR ( 'NONE', #100110, 1000.000000000000000 ) ;
#42724=ORIENTED_EDGE ( 'NONE', *, *, #38780, .F. ) ;
#42738=EDGE_LOOP ( 'NONE', ( #39060, #19114, #32977, #38481 ) ) ;
#42860=EDGE_LOOP ( 'NONE', ( #84731, #19635, #85238, #78021 ) ) ;
#42900=CARTESIAN_POINT ( 'NONE',  ( -8.376690734369036662, 11.49999999999999645, 2.100000000000000089 ) ) ;
#42925=CIRCLE ( 'NONE', #21810, 0.8500000000000017542 ) ;
#42991=DIRECTION ( 'NONE',  ( -1.000000000000000000, 0.000000000000000000, 0.000000000000000000 ) ) ;
#43056=CARTESIAN_POINT ( 'NONE',  ( 2.499999999999988454, 22.00000000000000000, 2.100000000000000089 ) ) ;
#43065=EDGE_LOOP ( 'NONE', ( #1329, #73290, #30199, #14055 ) ) ;
#43085=DIRECTION ( 'NONE',  ( 1.000000000000000000, 4.476705744456278313E-16, 0.000000000000000000 ) ) ;
#43092=CARTESIAN_POINT ( 'NONE',  ( -2.499999999999993339, 4.999999999999997335, 2.100000000000000089 ) ) ;
#43107=VERTEX_POINT ( 'NONE', #55256 ) ;
#43128=LINE ( 'NONE', #65990, #33605 ) ;
#43218=ORIENTED_EDGE ( 'NONE', *, *, #11867, .T. ) ;
#43223=DIRECTION ( 'NONE',  ( -1.000000000000000000, 0.000000000000000000, 0.000000000000000000 ) ) ;
#43244=ORIENTED_EDGE ( 'NONE', *, *, #13657, .F. ) ;
#43342=ORIENTED_EDGE ( 'NONE', *, *, #51614, .F. ) ;
#43406=LINE ( 'NONE', #98161, #88398 ) ;
#43499=VECTOR ( 'NONE', #36657, 1000.000000000000114 ) ;
#43587=EDGE_CURVE ( 'NONE', #1165, #51313, #28016, .T. ) ;
#43631=DIRECTION ( 'NONE',  ( -0.000000000000000000, -0.000000000000000000, -1.000000000000000000 ) ) ;
#43641=CARTESIAN_POINT ( 'NONE',  ( -8.749999999999767297, 18.74999999999999645, 0.000000000000000000 ) ) ;
#43689=ORIENTED_EDGE ( 'NONE', *, *, #17714, .T. ) ;
#43723=CARTESIAN_POINT ( 'NONE',  ( -10.34999999999999254, 3.983606557377048940, 3.319672131147540561 ) ) ;
#43802=ORIENTED_EDGE ( 'NONE', *, *, #23191, .F. ) ;
#43803=DIRECTION ( 'NONE',  ( -1.250792852327444499E-32, -1.571307496355802709E-16, -1.000000000000000000 ) ) ;
#43807=FACE_OUTER_BOUND ( 'NONE', #67422, .T. ) ;
#43819=ORIENTED_EDGE ( 'NONE', *, *, #90665, .T. ) ;
#43852=LINE ( 'NONE', #80910, #74477 ) ;
#43924=EDGE_LOOP ( 'NONE', ( #2686, #14526, #95868, #36551 ) ) ;
#43935=CARTESIAN_POINT ( 'NONE',  ( -9.299999999999991829, 12.00000000000002309, 2.100000000000000089 ) ) ;
#43954=ORIENTED_EDGE ( 'NONE', *, *, #11130, .F. ) ;
#44043=CARTESIAN_POINT ( 'NONE',  ( 10.34999999999999432, 12.00000000000002309, 0.000000000000000000 ) ) ;
#44059=EDGE_LOOP ( 'NONE', ( #2795, #87253, #48599, #76999 ) ) ;
#44066=ORIENTED_EDGE ( 'NONE', *, *, #65048, .F. ) ;
#44068=DIRECTION ( 'NONE',  ( -7.960204194457801640E-17, -1.000000000000000000, 0.000000000000000000 ) ) ;
#44102=VECTOR ( 'NONE', #32041, 1000.000000000000000 ) ;
#44122=PLANE ( 'NONE',  #9025 ) ;
#44170=VECTOR ( 'NONE', #39536, 1000.000000000000000 ) ;
#44371=PLANE ( 'NONE',  #48208 ) ;
#44402=CARTESIAN_POINT ( 'NONE',  ( 7.749999999999998224, 24.84999999999999787, 0.000000000000000000 ) ) ;
#44425=DIRECTION ( 'NONE',  ( -0.7071067811865516806, -0.7071067811865434649, 0.000000000000000000 ) ) ;
#44480=DIRECTION ( 'NONE',  ( -0.000000000000000000, -0.000000000000000000, -1.000000000000000000 ) ) ;
#44535=ORIENTED_EDGE ( 'NONE', *, *, #48197, .T. ) ;
#44584=LINE ( 'NONE', #59311, #4866 ) ;
#44627=CARTESIAN_POINT ( 'NONE',  ( -6.499999999999992895, 3.299745742347187193E-16, 2.100000000000000977 ) ) ;
#44685=CARTESIAN_POINT ( 'NONE',  ( -8.376690734369036662, 12.50000000000004974, 0.000000000000000000 ) ) ;
#44698=CARTESIAN_POINT ( 'NONE',  ( 10.34999999999999254, 2.573529411764703845, 1.544117647058823151 ) ) ;
#44734=VECTOR ( 'NONE', #40514, 1000.000000000000000 ) ;
#44735=EDGE_CURVE ( 'NONE', #27813, #19391, #78453, .T. ) ;
#44771=DIRECTION ( 'NONE',  ( -1.000000000000000000, -4.476705744456278313E-16, 0.000000000000000000 ) ) ;
#44870=DIRECTION ( 'NONE',  ( 0.000000000000000000, -0.000000000000000000, 1.000000000000000000 ) ) ;
#44913=EDGE_CURVE ( 'NONE', #86, #29751, #81553, .T. ) ;
#44915=DIRECTION ( 'NONE',  ( 1.000000000000000000, -1.734723475976800981E-15, 0.000000000000000000 ) ) ;
#44954=DIRECTION ( 'NONE',  ( 0.000000000000000000, -0.000000000000000000, -1.000000000000000000 ) ) ;
#44984=EDGE_CURVE ( 'NONE', #30443, #75862, #38276, .T. ) ;
#44986=VECTOR ( 'NONE', #5773, 1000.000000000000000 ) ;
#44999=CARTESIAN_POINT ( 'NONE',  ( 2.499999999999988454, 22.00000000000000000, 2.100000000000000089 ) ) ;
#45029=DIRECTION ( 'NONE',  ( -0.000000000000000000, -0.000000000000000000, -1.000000000000000000 ) ) ;
#45132=DIRECTION ( 'NONE',  ( 0.000000000000000000, -0.000000000000000000, -1.000000000000000000 ) ) ;
#45175=DIRECTION ( 'NONE',  ( -0.000000000000000000, -0.000000000000000000, -1.000000000000000000 ) ) ;
#45204=DIRECTION ( 'NONE',  ( 1.000000000000000000, -1.734723475976800981E-15, 0.000000000000000000 ) ) ;
#45217=ORIENTED_EDGE ( 'NONE', *, *, #28845, .F. ) ;
#45247=CIRCLE ( 'NONE', #69510, 0.8500000000000017542 ) ;
#45264=CARTESIAN_POINT ( 'NONE',  ( 7.749999999999998224, 24.84999999999999787, 2.100000000000000089 ) ) ;
#45276=DIRECTION ( 'NONE',  ( -1.000000000000000000, 5.782411586589363555E-16, 0.000000000000000000 ) ) ;
#45315=LINE ( 'NONE', #61039, #2314 ) ;
#45369=AXIS2_PLACEMENT_3D ( 'NONE', #83351, #81866, #26920 ) ;
#45413=VECTOR ( 'NONE', #81517, 1000.000000000000000 ) ;
#45497=ORIENTED_EDGE ( 'NONE', *, *, #16879, .F. ) ;
#45522=CARTESIAN_POINT ( 'NONE',  ( 3.737436867076077363, 13.63388347648318444, 2.100000000000000089 ) ) ;
#45870=EDGE_CURVE ( 'NONE', #17884, #94189, #58948, .T. ) ;
#46002=CARTESIAN_POINT ( 'NONE',  ( -8.499999999999987566, 18.74999999999999645, 2.100000000000000089 ) ) ;
#46013=CARTESIAN_POINT ( 'NONE',  ( -8.499999999999987566, 18.99999999999977973, 2.100000000000000089 ) ) ;
#46022=DIRECTION ( 'NONE',  ( -3.389844910009033029E-15, 1.000000000000000000, 0.000000000000000000 ) ) ;
#46149=VECTOR ( 'NONE', #85425, 1000.000000000000000 ) ;
#46205=ORIENTED_EDGE ( 'NONE', *, *, #95726, .F. ) ;
#46214=ORIENTED_EDGE ( 'NONE', *, *, #62720, .F. ) ;
#46265=CARTESIAN_POINT ( 'NONE',  ( 10.34999999999999432, 12.00000000000002309, 2.100000000000000089 ) ) ;
#46446=CARTESIAN_POINT ( 'NONE',  ( -10.34999999999999254, 1.999999999999999112, 2.499999999999999112 ) ) ;
#46486=EDGE_LOOP ( 'NONE', ( #73747, #68763, #86366, #94116 ) ) ;
#46497=CIRCLE ( 'NONE', #82136, 1.249999999999997558 ) ;
#46510=CARTESIAN_POINT ( 'NONE',  ( 2.899999999999999023, 33.29999999999999716, 2.100000000000000089 ) ) ;
#46529=( LENGTH_UNIT ( ) NAMED_UNIT ( * ) SI_UNIT ( .MILLI., .METRE. ) );
#46545=ORIENTED_EDGE ( 'NONE', *, *, #25605, .T. ) ;
#46551=EDGE_CURVE ( 'NONE', #70905, #57983, #16969, .T. ) ;
#46576=CARTESIAN_POINT ( 'NONE',  ( -2.499999999999986677, 22.00000000000000000, 2.100000000000000089 ) ) ;
#46675=PLANE ( 'NONE',  #78884 ) ;
#46717=EDGE_CURVE ( 'NONE', #80526, #17884, #45315, .T. ) ;
#46813=ORIENTED_EDGE ( 'NONE', *, *, #33624, .T. ) ;
#46849=LINE ( 'NONE', #31109, #97815 ) ;
#46877=CIRCLE ( 'NONE', #64737, 10.80000000000000782 ) ;
#46881=VECTOR ( 'NONE', #35069, 1000.000000000000000 ) ;
#47022=VECTOR ( 'NONE', #3271, 1000.000000000000000 ) ;
#47089=DIRECTION ( 'NONE',  ( 1.000000000000000000, 0.000000000000000000, 0.000000000000000000 ) ) ;
#47140=DIRECTION ( 'NONE',  ( -0.000000000000000000, -0.000000000000000000, -1.000000000000000000 ) ) ;
#47229=DIRECTION ( 'NONE',  ( 0.000000000000000000, -0.000000000000000000, -1.000000000000000000 ) ) ;
#47240=DIRECTION ( 'NONE',  ( 3.469446951953611033E-15, 1.000000000000000000, 0.000000000000000000 ) ) ;
#47430=DIRECTION ( 'NONE',  ( 1.000000000000000000, 0.000000000000000000, 0.000000000000000000 ) ) ;
#47439=DIRECTION ( 'NONE',  ( 0.000000000000000000, 0.000000000000000000, 1.000000000000000000 ) ) ;
#47483=PLANE ( 'NONE',  #97589 ) ;
#47572=ORIENTED_EDGE ( 'NONE', *, *, #63550, .F. ) ;
#47587=VERTEX_POINT ( 'NONE', #14992 ) ;
#47718=DIRECTION ( 'NONE',  ( 1.000000000000000000, -7.960204194457801640E-17, 0.000000000000000000 ) ) ;
#47721=VERTEX_POINT ( 'NONE', #24100 ) ;
#47723=VERTEX_POINT ( 'NONE', #16482 ) ;
#47776=CARTESIAN_POINT ( 'NONE',  ( -6.499999999999992895, -1.517883041479705813E-15, 3.499999999999998224 ) ) ;
#47802=VECTOR ( 'NONE', #45276, 1000.000000000000000 ) ;
#47856=VECTOR ( 'NONE', #40943, 1000.000000000000000 ) ;
#47872=CARTESIAN_POINT ( 'NONE',  ( -8.499999999999987566, 18.74999999999999645, 2.100000000000000089 ) ) ;
#47874=ORIENTED_EDGE ( 'NONE', *, *, #3654, .F. ) ;
#47879=EDGE_CURVE ( 'NONE', #15338, #15222, #23459, .T. ) ;
#47921=CARTESIAN_POINT ( 'NONE',  ( -6.499999999999992895, 1.999999999999999112, 3.499999999999999112 ) ) ;
#47941=CARTESIAN_POINT ( 'NONE',  ( 6.499999999999992895, -5.174132726397565334E-16, 0.000000000000000000 ) ) ;
#47972=CARTESIAN_POINT ( 'NONE',  ( 2.499999999999988454, 22.00000000000000000, 0.000000000000000000 ) ) ;
#47989=AXIS2_PLACEMENT_3D ( 'NONE', #25359, #18252, #33979 ) ;
#48102=DIRECTION ( 'NONE',  ( 0.000000000000000000, 0.000000000000000000, 1.000000000000000000 ) ) ;
#48189=ORIENTED_EDGE ( 'NONE', *, *, #91344, .F. ) ;
#48197=EDGE_CURVE ( 'NONE', #49615, #36274, #19949, .T. ) ;
#48208=AXIS2_PLACEMENT_3D ( 'NONE', #98130, #90039, #44870 ) ;
#48220=CARTESIAN_POINT ( 'NONE',  ( 2.899999999999999467, 33.29999999999999716, 0.000000000000000000 ) ) ;
#48269=VERTEX_POINT ( 'NONE', #13743 ) ;
#48293=CARTESIAN_POINT ( 'NONE',  ( -9.299999999999991829, 12.00000000000002309, 2.100000000000000089 ) ) ;
#48309=EDGE_CURVE ( 'NONE', #99197, #70905, #79930, .T. ) ;
#48375=DIRECTION ( 'NONE',  ( 1.000000000000000000, 0.000000000000000000, 0.000000000000000000 ) ) ;
#48403=AXIS2_PLACEMENT_3D ( 'NONE', #39644, #70600, #32035 ) ;
#48405=EDGE_CURVE ( 'NONE', #65034, #58206, #529, .T. ) ;
#48517=EDGE_CURVE ( 'NONE', #33604, #94189, #72555, .T. ) ;
#48523=LINE ( 'NONE', #93670, #59818 ) ;
#48599=ORIENTED_EDGE ( 'NONE', *, *, #579, .T. ) ;
#48622=CARTESIAN_POINT ( 'NONE',  ( 6.499999999999992895, 4.999999999999998224, 2.100000000000000089 ) ) ;
#48663=EDGE_CURVE ( 'NONE', #64945, #6225, #18368, .T. ) ;
#48675=DIRECTION ( 'NONE',  ( -0.000000000000000000, -0.000000000000000000, -1.000000000000000000 ) ) ;
#48684=CARTESIAN_POINT ( 'NONE',  ( -3.749999999999999112, 25.69999999999999574, 0.000000000000000000 ) ) ;
#48692=DIRECTION ( 'NONE',  ( -0.7071067811865515695, 0.7071067811865435759, 0.000000000000000000 ) ) ;
#48788=CARTESIAN_POINT ( 'NONE',  ( 8.499999999999989342, 18.74999999999999645, 2.100000000000000089 ) ) ;
#48830=CARTESIAN_POINT ( 'NONE',  ( 8.676776695296462449, 18.57322330470351091, 2.100000000000000089 ) ) ;
#48878=EDGE_CURVE ( 'NONE', #26341, #50456, #78018, .T. ) ;
#48950=CARTESIAN_POINT ( 'NONE',  ( -7.749999999999996447, 24.84999999999999787, 2.100000000000000089 ) ) ;
#48978=ORIENTED_EDGE ( 'NONE', *, *, #54588, .F. ) ;
#48994=EDGE_LOOP ( 'NONE', ( #80621, #89239, #46813, #56056, #84964, #42465, #64756, #35455, #25376, #5526, #75694, #51564, #84132, #56401, #59069, #60799, #40576, #87270, #34461, #66226, #63289, #33600, #74087, #89892, #16189, #59188, #27507, #81726, #86618, #29100, #42223, #93966, #96498, #67795, #70682, #14404, #38665, #70365, #75421, #82801, #23577, #25970, #89037, #1594, #46205, #12076, #84244, #53063, #3769, #21893 ) ) ;
#49221=EDGE_CURVE ( 'NONE', #9489, #43107, #46849, .T. ) ;
#49231=CARTESIAN_POINT ( 'NONE',  ( -8.499999999999987566, 18.74999999999999645, 0.000000000000000000 ) ) ;
#49268=ORIENTED_EDGE ( 'NONE', *, *, #80585, .T. ) ;
#49337=PLANE ( 'NONE',  #1260 ) ;
#49348=EDGE_CURVE ( 'NONE', #47587, #75526, #24997, .T. ) ;
#49474=CARTESIAN_POINT ( 'NONE',  ( 10.34999999999999254, 4.999999999999998224, 0.000000000000000000 ) ) ;
#49505=CARTESIAN_POINT ( 'NONE',  ( -7.749999999999996447, 24.84999999999999787, 0.000000000000000000 ) ) ;
#49535=VECTOR ( 'NONE', #75620, 1000.000000000000114 ) ;
#49609=DIRECTION ( 'NONE',  ( 0.000000000000000000, -0.000000000000000000, -1.000000000000000000 ) ) ;
#49615=VERTEX_POINT ( 'NONE', #58782 ) ;
#49693=EDGE_CURVE ( 'NONE', #70905, #51313, #96837, .T. ) ;
#49735=AXIS2_PLACEMENT_3D ( 'NONE', #6981, #91211, #68878 ) ;
#49769=DIRECTION ( 'NONE',  ( 3.389844910009033029E-15, -1.000000000000000000, 0.000000000000000000 ) ) ;
#49786=ORIENTED_EDGE ( 'NONE', *, *, #7607, .F. ) ;
#49851=EDGE_LOOP ( 'NONE', ( #94493, #49786, #3900, #14888 ) ) ;
#49884=VERTEX_POINT ( 'NONE', #77476 ) ;
#49997=DIRECTION ( 'NONE',  ( -1.000000000000000000, 0.000000000000000000, 0.000000000000000000 ) ) ;
#50078=VECTOR ( 'NONE', #70919, 1000.000000000000000 ) ;
#50080=EDGE_CURVE ( 'NONE', #57247, #85245, #21433, .T. ) ;
#50143=CARTESIAN_POINT ( 'NONE',  ( -3.749999999999999112, 25.69999999999999574, 0.000000000000000000 ) ) ;
#50170=CARTESIAN_POINT ( 'NONE',  ( -10.34999999999997833, 22.00000000000000000, 0.000000000000000000 ) ) ;
#50225=VECTOR ( 'NONE', #23375, 1000.000000000000000 ) ;
#50241=EDGE_CURVE ( 'NONE', #56196, #32160, #7722, .T. ) ;
#50329=DIRECTION ( 'NONE',  ( -1.000000000000000000, -1.413818403454611288E-16, 0.000000000000000000 ) ) ;
#50358=ORIENTED_EDGE ( 'NONE', *, *, #84226, .T. ) ;
#50408=VECTOR ( 'NONE', #54990, 1000.000000000000000 ) ;
#50410=PLANE ( 'NONE',  #90674 ) ;
#50455=VERTEX_POINT ( 'NONE', #11233 ) ;
#50456=VERTEX_POINT ( 'NONE', #88869 ) ;
#50547=AXIS2_PLACEMENT_3D ( 'NONE', #38535, #70999, #472 ) ;
#50580=ORIENTED_EDGE ( 'NONE', *, *, #72369, .F. ) ;
#50583=VERTEX_POINT ( 'NONE', #28442 ) ;
#50650=ORIENTED_EDGE ( 'NONE', *, *, #76895, .T. ) ;
#50694=ORIENTED_EDGE ( 'NONE', *, *, #9694, .T. ) ;
#50780=LINE ( 'NONE', #66027, #32117 ) ;
#50921=SHAPE_REPRESENTATION ( 'Spring-loaded Plate_Varsay\X2\0131\X0\lan', ( #37391 ), #27759 ) ;
#50924=CARTESIAN_POINT ( 'NONE',  ( 6.499999999999992895, -1.874386984050377894E-16, 2.100000000000000977 ) ) ;
#51014=CARTESIAN_POINT ( 'NONE',  ( 8.499999999999989342, 18.74999999999999645, 0.000000000000000000 ) ) ;
#51030=VECTOR ( 'NONE', #51400, 1000.000000000000000 ) ;
#51065=ORIENTED_EDGE ( 'NONE', *, *, #81234, .T. ) ;
#51161=DIRECTION ( 'NONE',  ( 1.000000000000000000, -7.960204194457801640E-17, 0.000000000000000000 ) ) ;
#51172=CIRCLE ( 'NONE', #85206, 1.249999999999997558 ) ;
#51184=ORIENTED_EDGE ( 'NONE', *, *, #13101, .T. ) ;
#51197=EDGE_LOOP ( 'NONE', ( #70031, #81041, #62892, #56052, #31066, #72434, #83010, #95801 ) ) ;
#51242=ORIENTED_EDGE ( 'NONE', *, *, #21644, .T. ) ;
#51251=ORIENTED_EDGE ( 'NONE', *, *, #73199, .T. ) ;
#51313=VERTEX_POINT ( 'NONE', #72416 ) ;
#51374=CARTESIAN_POINT ( 'NONE',  ( 6.499999999999992895, 0.9999999999999993339, 1.084202172485504187E-16 ) ) ;
#51400=DIRECTION ( 'NONE',  ( -0.7071067811865516806, -0.7071067811865434649, 0.000000000000000000 ) ) ;
#51437=FACE_OUTER_BOUND ( 'NONE', #16117, .T. ) ;
#51495=FACE_OUTER_BOUND ( 'NONE', #84125, .T. ) ;
#51544=DIRECTION ( 'NONE',  ( 1.000000000000000000, 0.000000000000000000, 0.000000000000000000 ) ) ;
#51564=ORIENTED_EDGE ( 'NONE', *, *, #74322, .F. ) ;
#51577=ORIENTED_EDGE ( 'NONE', *, *, #50241, .T. ) ;
#51614=EDGE_CURVE ( 'NONE', #34532, #17884, #72287, .T. ) ;
#51663=LINE ( 'NONE', #22182, #17836 ) ;
#51682=ORIENTED_EDGE ( 'NONE', *, *, #76895, .F. ) ;
#51688=PLANE ( 'NONE',  #33638 ) ;
#51717=ADVANCED_FACE ( 'NONE', ( #17989 ), #66191, .F. ) ;
#51734=AXIS2_PLACEMENT_3D ( 'NONE', #24861, #47718, #10145 ) ;
#51798=DIRECTION ( 'NONE',  ( -0.000000000000000000, 0.000000000000000000, 1.000000000000000000 ) ) ;
#51904=CARTESIAN_POINT ( 'NONE',  ( -8.499999999999987566, 18.99999999999977973, 2.100000000000000089 ) ) ;
#52010=DIRECTION ( 'NONE',  ( -0.000000000000000000, -0.000000000000000000, -1.000000000000000000 ) ) ;
#52108=EDGE_CURVE ( 'NONE', #34532, #33604, #72126, .T. ) ;
#52218=CARTESIAN_POINT ( 'NONE',  ( 4.621320343559619737, 12.50000000000004974, 2.100000000000000089 ) ) ;
#52276=ORIENTED_EDGE ( 'NONE', *, *, #7638, .T. ) ;
#52299=AXIS2_PLACEMENT_3D ( 'NONE', #86809, #9689, #1589 ) ;
#52413=CARTESIAN_POINT ( 'NONE',  ( 4.621320343559619737, 12.50000000000004974, 2.100000000000000089 ) ) ;
#52484=EDGE_LOOP ( 'NONE', ( #97869, #71445, #71397, #71677 ) ) ;
#52567=CARTESIAN_POINT ( 'NONE',  ( 2.499999999999988454, 22.00000000000000000, 2.100000000000000089 ) ) ;
#52570=DIRECTION ( 'NONE',  ( 0.000000000000000000, 0.5144957554275265688, -0.8574929257125440962 ) ) ;
#52617=EDGE_CURVE ( 'NONE', #85384, #14389, #30733, .T. ) ;
#52630=EDGE_CURVE ( 'NONE', #62142, #53704, #75900, .T. ) ;
#52714=CARTESIAN_POINT ( 'NONE',  ( 7.749999999999998224, 25.69999999999999574, 2.100000000000000089 ) ) ;
#52717=DIRECTION ( 'NONE',  ( -1.000000000000000000, 0.000000000000000000, 0.000000000000000000 ) ) ;
#52726=CARTESIAN_POINT ( 'NONE',  ( 6.499999999999992895, 1.999999999999998668, 0.000000000000000000 ) ) ;
#52736=CARTESIAN_POINT ( 'NONE',  ( -1.751198251822016161, 22.56127314141087581, 0.000000000000000000 ) ) ;
#52764=AXIS2_PLACEMENT_3D ( 'NONE', #43935, #24077, #47430 ) ;
#52772=DIRECTION ( 'NONE',  ( -0.000000000000000000, -0.000000000000000000, -1.000000000000000000 ) ) ;
#52787=CARTESIAN_POINT ( 'NONE',  ( -10.34999999999999254, 2.239999999999997105, 2.100000000000000977 ) ) ;
#52803=AXIS2_PLACEMENT_3D ( 'NONE', #48293, #16326, #92443 ) ;
#52829=VECTOR ( 'NONE', #55294, 1000.000000000000000 ) ;
#52851=LINE ( 'NONE', #53360, #50225 ) ;
#52954=ORIENTED_EDGE ( 'NONE', *, *, #86185, .F. ) ;
#52992=ORIENTED_EDGE ( 'NONE', *, *, #23077, .F. ) ;
#53063=ORIENTED_EDGE ( 'NONE', *, *, #26995, .F. ) ;
#53155=( NAMED_UNIT ( * ) PLANE_ANGLE_UNIT ( ) SI_UNIT ( $, .RADIAN. ) );
#53179=ORIENTED_EDGE ( 'NONE', *, *, #96536, .F. ) ;
#53284=DIRECTION ( 'NONE',  ( -1.000000000000000000, 0.000000000000000000, 0.000000000000000000 ) ) ;
#53302=VERTEX_POINT ( 'NONE', #38714 ) ;
#53313=AXIS2_PLACEMENT_3D ( 'NONE', #2462, #47140, #40529 ) ;
#53360=CARTESIAN_POINT ( 'NONE',  ( 10.34999999999998010, 27.69999999999999929, 2.100000000000000089 ) ) ;
#53384=LINE ( 'NONE', #70100, #35438 ) ;
#53406=AXIS2_PLACEMENT_3D ( 'NONE', #58578, #20494, #73794 ) ;
#53407=CARTESIAN_POINT ( 'NONE',  ( 10.34999999999999254, 4.999999999999998224, 0.000000000000000000 ) ) ;
#53456=CIRCLE ( 'NONE', #72871, 0.2500000000000011102 ) ;
#53528=CARTESIAN_POINT ( 'NONE',  ( 4.621320343559625066, 12.75000000000004974, 0.000000000000000000 ) ) ;
#53558=ORIENTED_EDGE ( 'NONE', *, *, #40169, .F. ) ;
#53592=CARTESIAN_POINT ( 'NONE',  ( -6.499999999999992895, 2.239999999999997105, 2.100000000000000977 ) ) ;
#53616=DIRECTION ( 'NONE',  ( -0.000000000000000000, -0.000000000000000000, -1.000000000000000000 ) ) ;
#53702=ADVANCED_FACE ( 'NONE', ( #69380 ), #15088, .F. ) ;
#53704=VERTEX_POINT ( 'NONE', #14079 ) ;
#53766=CIRCLE ( 'NONE', #76405, 1.050000000000000488 ) ;
#53787=DIRECTION ( 'NONE',  ( 1.000000000000000000, 0.000000000000000000, 0.000000000000000000 ) ) ;
#53972=EDGE_LOOP ( 'NONE', ( #23331, #80164, #70289, #63383 ) ) ;
#53975=ORIENTED_EDGE ( 'NONE', *, *, #77430, .T. ) ;
#54024=ADVANCED_FACE ( 'NONE', ( #83671 ), #44122, .T. ) ;
#54046=DIRECTION ( 'NONE',  ( -0.000000000000000000, -0.000000000000000000, -1.000000000000000000 ) ) ;
#54149=EDGE_CURVE ( 'NONE', #74171, #53302, #33889, .T. ) ;
#54167=EDGE_CURVE ( 'NONE', #30443, #73380, #73455, .T. ) ;
#54249=LINE ( 'NONE', #44627, #37327 ) ;
#54295=DIRECTION ( 'NONE',  ( 0.000000000000000000, -0.000000000000000000, -1.000000000000000000 ) ) ;
#54296=VECTOR ( 'NONE', #79218, 1000.000000000000000 ) ;
#54298=LINE ( 'NONE', #85226, #11238 ) ;
#54304=VECTOR ( 'NONE', #74273, 1000.000000000000000 ) ;
#54464=ORIENTED_EDGE ( 'NONE', *, *, #26253, .T. ) ;
#54478=CYLINDRICAL_SURFACE ( 'NONE', #3367, 1.050000000000000488 ) ;
#54487=LINE ( 'NONE', #69718, #46149 ) ;
#54494=AXIS2_PLACEMENT_3D ( 'NONE', #86719, #79103, #79607 ) ;
#54568=EDGE_CURVE ( 'NONE', #62223, #20563, #32635, .T. ) ;
#54581=LINE ( 'NONE', #47972, #33492 ) ;
#54588=EDGE_CURVE ( 'NONE', #5782, #94189, #8804, .T. ) ;
#54607=CIRCLE ( 'NONE', #95165, 1.000000000000000444 ) ;
#54663=LINE ( 'NONE', #69377, #30629 ) ;
#54959=FACE_OUTER_BOUND ( 'NONE', #91379, .T. ) ;
#54990=DIRECTION ( 'NONE',  ( 7.960204194457801640E-17, 1.000000000000000000, 0.000000000000000000 ) ) ;
#55056=FACE_OUTER_BOUND ( 'NONE', #81144, .T. ) ;
#55063=DIRECTION ( 'NONE',  ( 7.960204194457801640E-17, 1.000000000000000000, 0.000000000000000000 ) ) ;
#55071=ADVANCED_FACE ( 'NONE', ( #77675 ), #89313, .T. ) ;
#55113=EDGE_CURVE ( 'NONE', #47587, #85757, #94985, .T. ) ;
#55152=CYLINDRICAL_SURFACE ( 'NONE', #80441, 0.2500000000000011102 ) ;
#55255=LINE ( 'NONE', #61366, #23907 ) ;
#55256=CARTESIAN_POINT ( 'NONE',  ( 7.662324775236977636, 31.59999999999999787, 0.000000000000000000 ) ) ;
#55261=EDGE_LOOP ( 'NONE', ( #90345, #89256, #85378, #57084 ) ) ;
#55273=CARTESIAN_POINT ( 'NONE',  ( 8.376690734369038438, 11.49999999999999645, 2.100000000000000089 ) ) ;
#55279=FACE_OUTER_BOUND ( 'NONE', #13709, .T. ) ;
#55294=DIRECTION ( 'NONE',  ( 1.000000000000000000, 0.000000000000000000, 0.000000000000000000 ) ) ;
#55368=ORIENTED_EDGE ( 'NONE', *, *, #79693, .F. ) ;
#55418=VECTOR ( 'NONE', #86290, 1000.000000000000000 ) ;
#55433=DIRECTION ( 'NONE',  ( 0.000000000000000000, -0.000000000000000000, -1.000000000000000000 ) ) ;
#55491=AXIS2_PLACEMENT_3D ( 'NONE', #55617, #86546, #78923 ) ;
#55506=DIRECTION ( 'NONE',  ( 0.000000000000000000, -0.000000000000000000, -1.000000000000000000 ) ) ;
#55545=AXIS2_PLACEMENT_3D ( 'NONE', #51014, #33782, #88077 ) ;
#55578=LINE ( 'NONE', #86508, #23103 ) ;
#55603=CARTESIAN_POINT ( 'NONE',  ( 9.552245033349362461E-16, 23.99999999999999645, 2.100000000000000089 ) ) ;
#55607=CARTESIAN_POINT ( 'NONE',  ( -9.383883476483159569, 17.86611652351680846, 2.100000000000000089 ) ) ;
#55617=CARTESIAN_POINT ( 'NONE',  ( -10.34999999999999254, -1.267509437117509414E-15, 2.100000000000000089 ) ) ;
#55619=CARTESIAN_POINT ( 'NONE',  ( -10.34999999999997833, 27.69999999999999929, 2.100000000000000089 ) ) ;
#55628=DIRECTION ( 'NONE',  ( 0.000000000000000000, -0.000000000000000000, -1.000000000000000000 ) ) ;
#55636=DIRECTION ( 'NONE',  ( -0.000000000000000000, -0.000000000000000000, -1.000000000000000000 ) ) ;
#55667=ORIENTED_EDGE ( 'NONE', *, *, #2908, .F. ) ;
#55779=VERTEX_POINT ( 'NONE', #86568 ) ;
#55783=CARTESIAN_POINT ( 'NONE',  ( 7.749999999999998224, 23.99999999999999289, 0.000000000000000000 ) ) ;
#55898=DIRECTION ( 'NONE',  ( 0.000000000000000000, -1.000000000000000000, -4.336808689942018722E-16 ) ) ;
#55949=CARTESIAN_POINT ( 'NONE',  ( -2.749999999999999112, 27.59999999999999432, 0.000000000000000000 ) ) ;
#55996=DIRECTION ( 'NONE',  ( -7.960204194457801640E-17, -1.000000000000000000, 1.571307496355802463E-16 ) ) ;
#56052=ORIENTED_EDGE ( 'NONE', *, *, #67527, .F. ) ;
#56053=LINE ( 'NONE', #10867, #71131 ) ;
#56056=ORIENTED_EDGE ( 'NONE', *, *, #40107, .T. ) ;
#56061=DIRECTION ( 'NONE',  ( 1.000000000000000000, 0.000000000000000000, 0.000000000000000000 ) ) ;
#56076=DIRECTION ( 'NONE',  ( -0.000000000000000000, -0.000000000000000000, -1.000000000000000000 ) ) ;
#56139=PLANE ( 'NONE',  #40762 ) ;
#56156=ORIENTED_EDGE ( 'NONE', *, *, #90223, .F. ) ;
#56184=CARTESIAN_POINT ( 'NONE',  ( -9.383883476483159569, 17.86611652351680846, 2.100000000000000089 ) ) ;
#56196=VERTEX_POINT ( 'NONE', #97919 ) ;
#56309=PRODUCT_DEFINITION_SHAPE ( 'NONE', 'NONE',  #70488 ) ;
#56322=ORIENTED_EDGE ( 'NONE', *, *, #31110, .T. ) ;
#56365=EDGE_CURVE ( 'NONE', #86751, #17712, #68486, .T. ) ;
#56401=ORIENTED_EDGE ( 'NONE', *, *, #86105, .F. ) ;
#56404=DIRECTION ( 'NONE',  ( -1.000000000000000000, 0.000000000000000000, 0.000000000000000000 ) ) ;
#56406=VECTOR ( 'NONE', #55063, 1000.000000000000000 ) ;
#56431=DIRECTION ( 'NONE',  ( 0.000000000000000000, -0.000000000000000000, -1.000000000000000000 ) ) ;
#56450=VERTEX_POINT ( 'NONE', #55273 ) ;
#56484=VERTEX_POINT ( 'NONE', #465 ) ;
#56557=EDGE_LOOP ( 'NONE', ( #69433, #24842, #8588, #377 ) ) ;
#56595=VECTOR ( 'NONE', #24065, 1000.000000000000000 ) ;
#56609=ORIENTED_EDGE ( 'NONE', *, *, #75870, .F. ) ;
#56633=DIRECTION ( 'NONE',  ( 1.000000000000000000, 0.000000000000000000, 0.000000000000000000 ) ) ;
#56809=VERTEX_POINT ( 'NONE', #68370 ) ;
#56830=ORIENTED_EDGE ( 'NONE', *, *, #96630, .T. ) ;
#56838=LINE ( 'NONE', #72057, #65832 ) ;
#56962=DIRECTION ( 'NONE',  ( -0.000000000000000000, 0.7682212795973760722, 0.6401843996644797086 ) ) ;
#56964=ADVANCED_FACE ( 'NONE', ( #71373 ), #55152, .F. ) ;
#57061=DIRECTION ( 'NONE',  ( -0.000000000000000000, -0.000000000000000000, -1.000000000000000000 ) ) ;
#57071=DIRECTION ( 'NONE',  ( -0.000000000000000000, -0.000000000000000000, -1.000000000000000000 ) ) ;
#57084=ORIENTED_EDGE ( 'NONE', *, *, #1557, .F. ) ;
#57086=ORIENTED_EDGE ( 'NONE', *, *, #63082, .F. ) ;
#57112=DIRECTION ( 'NONE',  ( -0.000000000000000000, -0.000000000000000000, -1.000000000000000000 ) ) ;
#57235=PLANE ( 'NONE',  #6135 ) ;
#57247=VERTEX_POINT ( 'NONE', #59145 ) ;
#57281=VERTEX_POINT ( 'NONE', #64609 ) ;
#57372=AXIS2_PLACEMENT_3D ( 'NONE', #11052, #57739, #42516 ) ;
#57454=DIRECTION ( 'NONE',  ( 1.000000000000000000, -7.960204194457801640E-17, 0.000000000000000000 ) ) ;
#57524=VERTEX_POINT ( 'NONE', #6659 ) ;
#57632=FACE_OUTER_BOUND ( 'NONE', #17146, .T. ) ;
#57717=VERTEX_POINT ( 'NONE', #20753 ) ;
#57739=DIRECTION ( 'NONE',  ( -0.000000000000000000, 0.000000000000000000, 1.000000000000000000 ) ) ;
#57787=CARTESIAN_POINT ( 'NONE',  ( -2.499999999999993339, 18.99999999999977618, 2.100000000000000089 ) ) ;
#57867=EDGE_CURVE ( 'NONE', #20563, #63176, #2693, .T. ) ;
#57871=LINE ( 'NONE', #71082, #36896 ) ;
#57904=DIRECTION ( 'NONE',  ( 0.000000000000000000, -0.000000000000000000, -1.000000000000000000 ) ) ;
#57923=ORIENTED_EDGE ( 'NONE', *, *, #4848, .F. ) ;
#57983=VERTEX_POINT ( 'NONE', #82793 ) ;
#58119=DIRECTION ( 'NONE',  ( 0.000000000000000000, 0.6401843996644797086, -0.7682212795973759611 ) ) ;
#58179=VERTEX_POINT ( 'NONE', #40128 ) ;
#58206=VERTEX_POINT ( 'NONE', #87805 ) ;
#58286=CARTESIAN_POINT ( 'NONE',  ( 8.676776695296466002, 18.57322330470350735, 0.000000000000000000 ) ) ;
#58355=ORIENTED_EDGE ( 'NONE', *, *, #49693, .T. ) ;
#58366=CARTESIAN_POINT ( 'NONE',  ( -2.499999999999993339, 18.99999999999977618, 0.000000000000000000 ) ) ;
#58368=ADVANCED_FACE ( 'NONE', ( #75550, #15161 ), #30892, .T. ) ;
#58374=PLANE ( 'NONE',  #82848 ) ;
#58390=EDGE_CURVE ( 'NONE', #31511, #64945, #22261, .T. ) ;
#58459=DIRECTION ( 'NONE',  ( 0.000000000000000000, -0.6401843996644797086, 0.7682212795973760722 ) ) ;
#58502=ORIENTED_EDGE ( 'NONE', *, *, #49693, .F. ) ;
#58503=LINE ( 'NONE', #19913, #92636 ) ;
#58535=FACE_OUTER_BOUND ( 'NONE', #79541, .T. ) ;
#58578=CARTESIAN_POINT ( 'NONE',  ( 4.621320343559625066, 12.75000000000004974, 2.100000000000000089 ) ) ;
#58605=CARTESIAN_POINT ( 'NONE',  ( -2.749999999999999112, 27.59999999999999432, 2.100000000000000089 ) ) ;
#58696=EDGE_LOOP ( 'NONE', ( #33244, #100312, #44535, #4657 ) ) ;
#58782=CARTESIAN_POINT ( 'NONE',  ( -3.737436867076076030, 13.63388347648318444, 2.100000000000000089 ) ) ;
#58784=FACE_OUTER_BOUND ( 'NONE', #93895, .T. ) ;
#58817=CARTESIAN_POINT ( 'NONE',  ( -2.499999999999993339, 19.99999999999999645, 2.100000000000000089 ) ) ;
#58849=DIRECTION ( 'NONE',  ( 1.000000000000000000, 1.655121434032223174E-15, 0.000000000000000000 ) ) ;
#58948=CIRCLE ( 'NONE', #57372, 1.000000000000000444 ) ;
#59003=ADVANCED_FACE ( 'NONE', ( #71604 ), #41661, .T. ) ;
#59014=LINE ( 'NONE', #28538, #4608 ) ;
#59029=VERTEX_POINT ( 'NONE', #88324 ) ;
#59069=ORIENTED_EDGE ( 'NONE', *, *, #34616, .F. ) ;
#59085=CYLINDRICAL_SURFACE ( 'NONE', #53406, 0.2500000000000011102 ) ;
#59145=CARTESIAN_POINT ( 'NONE',  ( -2.499999999999993339, 18.99999999999977618, 2.100000000000000089 ) ) ;
#59188=ORIENTED_EDGE ( 'NONE', *, *, #96536, .T. ) ;
#59192=VECTOR ( 'NONE', #62757, 1000.000000000000000 ) ;
#59226=VECTOR ( 'NONE', #94217, 1000.000000000000000 ) ;
#59265=LINE ( 'NONE', #29803, #17634 ) ;
#59285=ORIENTED_EDGE ( 'NONE', *, *, #54149, .F. ) ;
#59311=CARTESIAN_POINT ( 'NONE',  ( 3.750000000000001332, 25.69999999999999574, 2.100000000000000089 ) ) ;
#59385=DIRECTION ( 'NONE',  ( 0.000000000000000000, 0.000000000000000000, 1.000000000000000000 ) ) ;
#59394=CARTESIAN_POINT ( 'NONE',  ( -6.499999999999992895, -1.267509437117509414E-15, -2.500000000000001332 ) ) ;
#59418=EDGE_LOOP ( 'NONE', ( #39580, #3304, #78492, #78309, #6619 ) ) ;
#59419=LINE ( 'NONE', #44698, #49535 ) ;
#59444=EDGE_LOOP ( 'NONE', ( #69270, #16974, #46545, #37511 ) ) ;
#59494=DIRECTION ( 'NONE',  ( -0.000000000000000000, -0.000000000000000000, -1.000000000000000000 ) ) ;
#59539=ADVANCED_FACE ( 'NONE', ( #21398 ), #29522, .F. ) ;
#59545=EDGE_CURVE ( 'NONE', #11247, #24018, #76190, .T. ) ;
#59552=DIRECTION ( 'NONE',  ( -1.000000000000000000, 0.000000000000000000, 0.000000000000000000 ) ) ;
#59693=VERTEX_POINT ( 'NONE', #86520 ) ;
#59784=CARTESIAN_POINT ( 'NONE',  ( 2.499999999999995115, 19.99999999999999645, 0.000000000000000000 ) ) ;
#59818=VECTOR ( 'NONE', #55636, 1000.000000000000000 ) ;
#59832=ORIENTED_EDGE ( 'NONE', *, *, #9734, .T. ) ;
#59946=DIRECTION ( 'NONE',  ( -1.000000000000000000, 0.000000000000000000, 0.000000000000000000 ) ) ;
#59991=CIRCLE ( 'NONE', #97056, 0.8500000000000017542 ) ;
#60004=ORIENTED_EDGE ( 'NONE', *, *, #26995, .T. ) ;
#60077=ORIENTED_EDGE ( 'NONE', *, *, #43587, .F. ) ;
#60087=CARTESIAN_POINT ( 'NONE',  ( -10.34999999999997833, 22.00000000000000000, 2.100000000000000089 ) ) ;
#60185=DIRECTION ( 'NONE',  ( -1.000000000000000000, 0.000000000000000000, 0.000000000000000000 ) ) ;
#60254=VERTEX_POINT ( 'NONE', #91986 ) ;
#60287=DIRECTION ( 'NONE',  ( -0.000000000000000000, 0.000000000000000000, -1.000000000000000000 ) ) ;
#60301=ORIENTED_EDGE ( 'NONE', *, *, #31662, .T. ) ;
#60396=CIRCLE ( 'NONE', #2085, 0.2499999999997798983 ) ;
#60454=CARTESIAN_POINT ( 'NONE',  ( 8.499999999999989342, 18.74999999999999645, 2.100000000000000089 ) ) ;
#60497=VECTOR ( 'NONE', #33911, 1000.000000000000000 ) ;
#60501=DIRECTION ( 'NONE',  ( 1.000000000000000000, 0.000000000000000000, 0.000000000000000000 ) ) ;
#60505=EDGE_CURVE ( 'NONE', #62223, #57717, #19364, .T. ) ;
#60516=CARTESIAN_POINT ( 'NONE',  ( 8.349999999999972999, 27.69999999999999574, 2.100000000000000089 ) ) ;
#60576=ORIENTED_EDGE ( 'NONE', *, *, #27628, .F. ) ;
#60607=DIRECTION ( 'NONE',  ( -1.000000000000000000, 0.000000000000000000, 0.000000000000000000 ) ) ;
#60658=ORIENTED_EDGE ( 'NONE', *, *, #8768, .T. ) ;
#60689=DIRECTION ( 'NONE',  ( -0.000000000000000000, 0.000000000000000000, -1.000000000000000000 ) ) ;
#60758=ORIENTED_EDGE ( 'NONE', *, *, #11130, .T. ) ;
#60769=CARTESIAN_POINT ( 'NONE',  ( 3.750000000000001332, 25.69999999999999574, 2.100000000000000089 ) ) ;
#60790=CYLINDRICAL_SURFACE ( 'NONE', #97298, 1.050000000000000488 ) ;
#60797=EDGE_LOOP ( 'NONE', ( #29324, #29901, #70901, #30350 ) ) ;
#60799=ORIENTED_EDGE ( 'NONE', *, *, #78276, .F. ) ;
#60806=DIRECTION ( 'NONE',  ( -0.000000000000000000, 0.000000000000000000, -1.000000000000000000 ) ) ;
#60946=ORIENTED_EDGE ( 'NONE', *, *, #17143, .T. ) ;
#61005=EDGE_CURVE ( 'NONE', #89308, #8902, #77889, .T. ) ;
#61008=ORIENTED_EDGE ( 'NONE', *, *, #81264, .T. ) ;
#61039=CARTESIAN_POINT ( 'NONE',  ( 3.750000000000001332, 25.69999999999999574, 0.000000000000000000 ) ) ;
#61087=VERTEX_POINT ( 'NONE', #10394 ) ;
#61133=ADVANCED_FACE ( 'NONE', ( #18009 ), #72808, .T. ) ;
#61197=FACE_OUTER_BOUND ( 'NONE', #51197, .T. ) ;
#61255=LINE ( 'NONE', #92177, #31564 ) ;
#61278=FACE_OUTER_BOUND ( 'NONE', #22732, .T. ) ;
#61351=CARTESIAN_POINT ( 'NONE',  ( 4.621320343559619737, 12.50000000000004974, 0.000000000000000000 ) ) ;
#61355=EDGE_CURVE ( 'NONE', #80660, #98207, #18928, .T. ) ;
#61366=CARTESIAN_POINT ( 'NONE',  ( 10.34999999999998010, 22.00000000000000000, 2.100000000000000089 ) ) ;
#61376=VECTOR ( 'NONE', #3720, 1000.000000000000000 ) ;
#61442=AXIS2_PLACEMENT_3D ( 'NONE', #20608, #82508, #52570 ) ;
#61524=FACE_OUTER_BOUND ( 'NONE', #46486, .T. ) ;
#61677=VERTEX_POINT ( 'NONE', #41 ) ;
#61678=CYLINDRICAL_SURFACE ( 'NONE', #20991, 1.000000000000000444 ) ;
#61700=CARTESIAN_POINT ( 'NONE',  ( 10.34999999999999254, 3.499999999999995115, 0.000000000000000000 ) ) ;
#61864=DIRECTION ( 'NONE',  ( 0.000000000000000000, -0.000000000000000000, -1.000000000000000000 ) ) ;
#61903=DIRECTION ( 'NONE',  ( 0.000000000000000000, -1.000000000000000000, 0.000000000000000000 ) ) ;
#61940=ORIENTED_EDGE ( 'NONE', *, *, #36640, .T. ) ;
#61974=AXIS2_PLACEMENT_3D ( 'NONE', #82419, #20024, #67720 ) ;
#62032=PLANE ( 'NONE',  #10603 ) ;
#62142=VERTEX_POINT ( 'NONE', #39493 ) ;
#62223=VERTEX_POINT ( 'NONE', #48622 ) ;
#62237=LINE ( 'NONE', #70843, #217 ) ;
#62346=ORIENTED_EDGE ( 'NONE', *, *, #39662, .F. ) ;
#62383=ADVANCED_FACE ( 'NONE', ( #28143 ), #44371, .T. ) ;
#62432=FACE_OUTER_BOUND ( 'NONE', #63211, .T. ) ;
#62538=VECTOR ( 'NONE', #47229, 1000.000000000000000 ) ;
#62651=ORIENTED_EDGE ( 'NONE', *, *, #86421, .F. ) ;
#62710=CARTESIAN_POINT ( 'NONE',  ( -4.444543648262984981, 12.92677669529668627, 2.100000000000000089 ) ) ;
#62720=EDGE_CURVE ( 'NONE', #85245, #55779, #82306, .T. ) ;
#62732=VECTOR ( 'NONE', #92008, 1000.000000000000000 ) ;
#62757=DIRECTION ( 'NONE',  ( 0.000000000000000000, 0.000000000000000000, 1.000000000000000000 ) ) ;
#62794=EDGE_CURVE ( 'NONE', #29229, #69616, #6664, .T. ) ;
#62796=LINE ( 'NONE', #369, #89981 ) ;
#62841=DIRECTION ( 'NONE',  ( 7.960204194457801640E-17, 1.000000000000000000, 2.891205793294678326E-16 ) ) ;
#62866=EDGE_CURVE ( 'NONE', #56809, #90981, #68575, .T. ) ;
#62892=ORIENTED_EDGE ( 'NONE', *, *, #2617, .T. ) ;
#62912=CYLINDRICAL_SURFACE ( 'NONE', #9080, 10.80000000000000782 ) ;
#62913=PLANE ( 'NONE',  #98635 ) ;
#62918=DIRECTION ( 'NONE',  ( 0.7071067811865435759, 0.7071067811865515695, -0.000000000000000000 ) ) ;
#63082=EDGE_CURVE ( 'NONE', #75990, #57717, #57871, .T. ) ;
#63104=VECTOR ( 'NONE', #8044, 1000.000000000000000 ) ;
#63176=VERTEX_POINT ( 'NONE', #35015 ) ;
#63205=DIRECTION ( 'NONE',  ( 1.000000000000000000, -7.960204194457801640E-17, 0.000000000000000000 ) ) ;
#63211=EDGE_LOOP ( 'NONE', ( #96918, #95948, #99209, #430 ) ) ;
#63240=CIRCLE ( 'NONE', #25990, 1.249999999999997558 ) ;
#63277=AXIS2_PLACEMENT_3D ( 'NONE', #78483, #24699, #17599 ) ;
#63289=ORIENTED_EDGE ( 'NONE', *, *, #32636, .T. ) ;
#63298=LINE ( 'NONE', #56184, #59226 ) ;
#63315=CARTESIAN_POINT ( 'NONE',  ( -6.499999999999992895, 4.999999999999999112, 2.100000000000000089 ) ) ;
#63321=ADVANCED_FACE ( 'NONE', ( #23263 ), #99396, .F. ) ;
#63367=DIRECTION ( 'NONE',  ( -7.960204194457801640E-17, -1.000000000000000000, 0.000000000000000000 ) ) ;
#63383=ORIENTED_EDGE ( 'NONE', *, *, #63603, .T. ) ;
#63407=VECTOR ( 'NONE', #81197, 1000.000000000000000 ) ;
#63447=DIRECTION ( 'NONE',  ( 0.000000000000000000, 0.000000000000000000, 1.000000000000000000 ) ) ;
#63550=EDGE_CURVE ( 'NONE', #10358, #34532, #764, .T. ) ;
#63582=ORIENTED_EDGE ( 'NONE', *, *, #93522, .F. ) ;
#63603=EDGE_CURVE ( 'NONE', #97853, #58206, #38822, .T. ) ;
#63616=LINE ( 'NONE', #92532, #50408 ) ;
#63721=DIRECTION ( 'NONE',  ( 0.000000000000000000, -0.000000000000000000, -1.000000000000000000 ) ) ;
#63748=ORIENTED_EDGE ( 'NONE', *, *, #62866, .F. ) ;
#63787=ADVANCED_FACE ( 'NONE', ( #76951 ), #70866, .F. ) ;
#63866=CARTESIAN_POINT ( 'NONE',  ( -2.749999999999999112, 26.59999999999999432, 2.100000000000000089 ) ) ;
#63900=EDGE_CURVE ( 'NONE', #36274, #73980, #59014, .T. ) ;
#64012=EDGE_CURVE ( 'NONE', #59693, #82244, #6203, .T. ) ;
#64022=VECTOR ( 'NONE', #75222, 1000.000000000000000 ) ;
#64137=DIRECTION ( 'NONE',  ( 1.000000000000000000, 0.000000000000000000, 0.000000000000000000 ) ) ;
#64221=AXIS2_PLACEMENT_3D ( 'NONE', #10955, #95690, #88584 ) ;
#64230=VERTEX_POINT ( 'NONE', #591 ) ;
#64405=ORIENTED_EDGE ( 'NONE', *, *, #36640, .F. ) ;
#64429=CARTESIAN_POINT ( 'NONE',  ( -8.676776695296460673, 18.57322330470351091, 2.100000000000000089 ) ) ;
#64471=ORIENTED_EDGE ( 'NONE', *, *, #35955, .F. ) ;
#64525=VECTOR ( 'NONE', #68540, 1000.000000000000000 ) ;
#64575=CARTESIAN_POINT ( 'NONE',  ( 2.499999999999993783, 4.999999999999997335, 2.100000000000000089 ) ) ;
#64589=EDGE_LOOP ( 'NONE', ( #19377, #43342, #91121, #82615 ) ) ;
#64603=EDGE_LOOP ( 'NONE', ( #44066, #91345, #4861, #93508 ) ) ;
#64609=CARTESIAN_POINT ( 'NONE',  ( -2.749999999999999112, 27.59999999999999432, 2.100000000000000089 ) ) ;
#64612=DIRECTION ( 'NONE',  ( 0.000000000000000000, 1.000000000000000000, 0.000000000000000000 ) ) ;
#64737=AXIS2_PLACEMENT_3D ( 'NONE', #37563, #51798, #84225 ) ;
#64756=ORIENTED_EDGE ( 'NONE', *, *, #88902, .T. ) ;
#64766=PLANE ( 'NONE',  #33691 ) ;
#64804=AXIS2_PLACEMENT_3D ( 'NONE', #74741, #19957, #36196 ) ;
#64852=CARTESIAN_POINT ( 'NONE',  ( 2.499999999999993783, 4.999999999999997335, 2.100000000000000089 ) ) ;
#64873=CARTESIAN_POINT ( 'NONE',  ( -10.34999999999999254, 12.00000000000002309, 2.100000000000000089 ) ) ;
#64928=FACE_OUTER_BOUND ( 'NONE', #43065, .T. ) ;
#64939=CARTESIAN_POINT ( 'NONE',  ( -2.499999999999993339, 19.99999999999999645, 2.100000000000000089 ) ) ;
#64945=VERTEX_POINT ( 'NONE', #72502 ) ;
#65030=LINE ( 'NONE', #9709, #11641 ) ;
#65034=VERTEX_POINT ( 'NONE', #97814 ) ;
#65048=EDGE_CURVE ( 'NONE', #50583, #37074, #59265, .T. ) ;
#65071=DIRECTION ( 'NONE',  ( 0.7071067811865516806, 0.7071067811865434649, 0.000000000000000000 ) ) ;
#65248=DIRECTION ( 'NONE',  ( 0.000000000000000000, 0.000000000000000000, 1.000000000000000000 ) ) ;
#65289=EDGE_CURVE ( 'NONE', #30127, #36030, #42440, .T. ) ;
#65351=DIRECTION ( 'NONE',  ( 1.000000000000000000, 0.000000000000000000, 0.000000000000000000 ) ) ;
#65378=VECTOR ( 'NONE', #74712, 1000.000000000000000 ) ;
#65412=VECTOR ( 'NONE', #24498, 1000.000000000000000 ) ;
#65419=LINE ( 'NONE', #34441, #52829 ) ;
#65464=CARTESIAN_POINT ( 'NONE',  ( -9.383883476483159569, 17.86611652351680846, 0.000000000000000000 ) ) ;
#65690=CARTESIAN_POINT ( 'NONE',  ( 3.750000000000001776, 26.59999999999999432, 2.100000000000000089 ) ) ;
#65713=FACE_OUTER_BOUND ( 'NONE', #29823, .T. ) ;
#65737=PLANE ( 'NONE',  #75755 ) ;
#65832=VECTOR ( 'NONE', #33471, 1000.000000000000000 ) ;
#65853=CARTESIAN_POINT ( 'NONE',  ( -10.34999999999997833, 27.69999999999999929, 2.100000000000000089 ) ) ;
#65922=VERTEX_POINT ( 'NONE', #35450 ) ;
#65968=ORIENTED_EDGE ( 'NONE', *, *, #78276, .T. ) ;
#65990=CARTESIAN_POINT ( 'NONE',  ( -10.34999999999999254, 1.999999999999999112, 3.499999999999999112 ) ) ;
#66027=CARTESIAN_POINT ( 'NONE',  ( 8.676776695296466002, 18.57322330470350735, 2.100000000000000089 ) ) ;
#66147=CARTESIAN_POINT ( 'NONE',  ( -2.749999999999999112, 27.59999999999999432, 2.100000000000000089 ) ) ;
#66191=CYLINDRICAL_SURFACE ( 'NONE', #4036, 0.8500000000000017542 ) ;
#66209=VERTEX_POINT ( 'NONE', #5487 ) ;
#66225=EDGE_LOOP ( 'NONE', ( #99454, #69123, #4074, #82591 ) ) ;
#66226=ORIENTED_EDGE ( 'NONE', *, *, #39662, .T. ) ;
#66276=LINE ( 'NONE', #74362, #85706 ) ;
#66297=EDGE_LOOP ( 'NONE', ( #47874, #43244, #3643, #4661 ) ) ;
#66382=AXIS2_PLACEMENT_3D ( 'NONE', #49231, #80159, #25366 ) ;
#66399=CARTESIAN_POINT ( 'NONE',  ( -10.34999999999999254, 4.999999999999999112, 2.100000000000000089 ) ) ;
#66413=EDGE_CURVE ( 'NONE', #56484, #88974, #63298, .T. ) ;
#66439=ORIENTED_EDGE ( 'NONE', *, *, #9734, .F. ) ;
#66445=EDGE_CURVE ( 'NONE', #99197, #1165, #9987, .T. ) ;
#66458=PLANE ( 'NONE',  #22029 ) ;
#66542=CARTESIAN_POINT ( 'NONE',  ( -10.34999999999999254, -1.517883041479705813E-15, 3.499999999999998224 ) ) ;
#66547=EDGE_LOOP ( 'NONE', ( #4635, #6648, #26760, #7258 ) ) ;
#66640=LINE ( 'NONE', #90442, #18680 ) ;
#66655=AXIS2_PLACEMENT_3D ( 'NONE', #68216, #36765, #28157 ) ;
#66706=EDGE_LOOP ( 'NONE', ( #2699, #11845, #72430, #51242 ) ) ;
#66728=VECTOR ( 'NONE', #71356, 1000.000000000000000 ) ;
#66733=CARTESIAN_POINT ( 'NONE',  ( -7.749999999999996447, 25.69999999999999574, 2.100000000000000089 ) ) ;
#66734=ORIENTED_EDGE ( 'NONE', *, *, #17882, .T. ) ;
#66783=CARTESIAN_POINT ( 'NONE',  ( 2.499999999999988454, 22.00000000000000000, 0.000000000000000000 ) ) ;
#66911=ORIENTED_EDGE ( 'NONE', *, *, #21172, .F. ) ;
#66964=EDGE_CURVE ( 'NONE', #55779, #76974, #95601, .T. ) ;
#67014=FACE_OUTER_BOUND ( 'NONE', #83859, .T. ) ;
#67160=FACE_OUTER_BOUND ( 'NONE', #93114, .T. ) ;
#67273=CARTESIAN_POINT ( 'NONE',  ( 8.499999999999989342, 18.74999999999999645, 2.100000000000000089 ) ) ;
#67308=ORIENTED_EDGE ( 'NONE', *, *, #48405, .T. ) ;
#67360=CARTESIAN_POINT ( 'NONE',  ( 2.499999999999993783, 4.999999999999997335, 0.000000000000000000 ) ) ;
#67399=CARTESIAN_POINT ( 'NONE',  ( -9.299999999999991829, 12.00000000000002309, 2.100000000000000089 ) ) ;
#67414=AXIS2_PLACEMENT_3D ( 'NONE', #28821, #36928, #60287 ) ;
#67422=EDGE_LOOP ( 'NONE', ( #67308, #90323, #75989, #60301 ) ) ;
#67445=LINE ( 'NONE', #52714, #2910 ) ;
#67470=VECTOR ( 'NONE', #82108, 1000.000000000000000 ) ;
#67527=EDGE_CURVE ( 'NONE', #63176, #30127, #59419, .T. ) ;
#67542=ORIENTED_EDGE ( 'NONE', *, *, #17455, .F. ) ;
#67563=ORIENTED_EDGE ( 'NONE', *, *, #38780, .T. ) ;
#67720=DIRECTION ( 'NONE',  ( -1.000000000000000000, 0.000000000000000000, -0.000000000000000000 ) ) ;
#67795=ORIENTED_EDGE ( 'NONE', *, *, #11867, .F. ) ;
#67846=LINE ( 'NONE', #18773, #18190 ) ;
#67879=VECTOR ( 'NONE', #28429, 1000.000000000000000 ) ;
#67942=CARTESIAN_POINT ( 'NONE',  ( -6.499999999999992895, 0.9999999999999993339, 3.499999999999998668 ) ) ;
#67956=CARTESIAN_POINT ( 'NONE',  ( 3.750000000000001332, 25.69999999999999574, 0.000000000000000000 ) ) ;
#68021=VERTEX_POINT ( 'NONE', #85214 ) ;
#68072=ORIENTED_EDGE ( 'NONE', *, *, #59545, .F. ) ;
#68168=VECTOR ( 'NONE', #8690, 1000.000000000000000 ) ;
#68216=CARTESIAN_POINT ( 'NONE',  ( 8.499999999999989342, 18.74999999999999645, 2.100000000000000089 ) ) ;
#68369=ADVANCED_FACE ( 'NONE', ( #61278 ), #76966, .T. ) ;
#68370=CARTESIAN_POINT ( 'NONE',  ( -2.499999999999993339, 19.99999999999999645, 2.100000000000000089 ) ) ;
#68373=LINE ( 'NONE', #38914, #80214 ) ;
#68417=ORIENTED_EDGE ( 'NONE', *, *, #39707, .T. ) ;
#68418=VECTOR ( 'NONE', #85660, 1000.000000000000000 ) ;
#68464=LINE ( 'NONE', #99399, #42553 ) ;
#68467=VECTOR ( 'NONE', #77426, 1000.000000000000000 ) ;
#68486=LINE ( 'NONE', #69487, #44170 ) ;
#68535=LINE ( 'NONE', #92861, #3277 ) ;
#68540=DIRECTION ( 'NONE',  ( 1.000000000000000000, -7.960204194457801640E-17, 0.000000000000000000 ) ) ;
#68575=LINE ( 'NONE', #69577, #80649 ) ;
#68597=CARTESIAN_POINT ( 'NONE',  ( -10.34999999999999254, 4.999999999999999112, 2.100000000000000089 ) ) ;
#68666=VERTEX_POINT ( 'NONE', #66783 ) ;
#68691=DIRECTION ( 'NONE',  ( -0.1736481776669261679, 0.9848077530122087975, 0.000000000000000000 ) ) ;
#68763=ORIENTED_EDGE ( 'NONE', *, *, #54149, .T. ) ;
#68849=DIRECTION ( 'NONE',  ( -1.000000000000000000, 0.000000000000000000, 0.000000000000000000 ) ) ;
#68878=DIRECTION ( 'NONE',  ( -1.000000000000000000, 0.000000000000000000, 0.000000000000000000 ) ) ;
#68889=ORIENTED_EDGE ( 'NONE', *, *, #72369, .T. ) ;
#69123=ORIENTED_EDGE ( 'NONE', *, *, #15883, .F. ) ;
#69164=ORIENTED_EDGE ( 'NONE', *, *, #44984, .T. ) ;
#69181=VERTEX_POINT ( 'NONE', #77215 ) ;
#69182=VECTOR ( 'NONE', #84666, 1000.000000000000000 ) ;
#69210=ORIENTED_EDGE ( 'NONE', *, *, #15917, .T. ) ;
#69270=ORIENTED_EDGE ( 'NONE', *, *, #83381, .F. ) ;
#69296=CARTESIAN_POINT ( 'NONE',  ( -2.899999999999996358, 33.29999999999999716, 2.100000000000000089 ) ) ;
#69365=CARTESIAN_POINT ( 'NONE',  ( 8.749999999999769074, 18.74999999999999645, 0.000000000000000000 ) ) ;
#69377=CARTESIAN_POINT ( 'NONE',  ( 6.499999999999992895, 2.573529411764703845, 1.544117647058822929 ) ) ;
#69380=FACE_OUTER_BOUND ( 'NONE', #93714, .T. ) ;
#69433=ORIENTED_EDGE ( 'NONE', *, *, #34616, .T. ) ;
#69455=CARTESIAN_POINT ( 'NONE',  ( -4.621320343559618848, 12.50000000000004974, 2.100000000000000089 ) ) ;
#69456=CARTESIAN_POINT ( 'NONE',  ( 3.737436867076077363, 13.63388347648318444, 2.100000000000000089 ) ) ;
#69487=CARTESIAN_POINT ( 'NONE',  ( -3.749999999999999112, 25.69999999999999574, 2.100000000000000089 ) ) ;
#69488=ORIENTED_EDGE ( 'NONE', *, *, #26671, .T. ) ;
#69507=CARTESIAN_POINT ( 'NONE',  ( -2.499999999999986677, 22.00000000000000000, 2.100000000000000089 ) ) ;
#69510=AXIS2_PLACEMENT_3D ( 'NONE', #44402, #52010, #99649 ) ;
#69577=CARTESIAN_POINT ( 'NONE',  ( -2.499999999999993339, 19.99999999999999645, 2.100000000000000089 ) ) ;
#69583=EDGE_CURVE ( 'NONE', #82244, #12412, #46877, .T. ) ;
#69616=VERTEX_POINT ( 'NONE', #44685 ) ;
#69622=CARTESIAN_POINT ( 'NONE',  ( -6.499999999999992895, 1.999999999999999112, 2.499999999999999112 ) ) ;
#69718=CARTESIAN_POINT ( 'NONE',  ( 4.621320343559255583, 11.49999999999999467, 2.100000000000000089 ) ) ;
#69732=CARTESIAN_POINT ( 'NONE',  ( -4.621320343559254695, 11.49999999999999645, 2.100000000000000089 ) ) ;
#69785=CARTESIAN_POINT ( 'NONE',  ( 2.899999999999999467, 31.80000000000000071, 2.100000000000000089 ) ) ;
#69787=FACE_OUTER_BOUND ( 'NONE', #43924, .T. ) ;
#69795=ORIENTED_EDGE ( 'NONE', *, *, #23077, .T. ) ;
#69825=DIRECTION ( 'NONE',  ( 7.960204194457801640E-17, 1.000000000000000000, 0.000000000000000000 ) ) ;
#69955=VECTOR ( 'NONE', #29282, 1000.000000000000000 ) ;
#70031=ORIENTED_EDGE ( 'NONE', *, *, #52617, .T. ) ;
#70079=CARTESIAN_POINT ( 'NONE',  ( 8.499999999999989342, 18.99999999999977973, 2.100000000000000089 ) ) ;
#70100=CARTESIAN_POINT ( 'NONE',  ( 9.552245033349362461E-16, 23.99999999999999645, 0.000000000000000000 ) ) ;
#70126=DIRECTION ( 'NONE',  ( -0.000000000000000000, -0.000000000000000000, -1.000000000000000000 ) ) ;
#70218=DIRECTION ( 'NONE',  ( 1.000000000000000000, 0.000000000000000000, 0.000000000000000000 ) ) ;
#70289=ORIENTED_EDGE ( 'NONE', *, *, #22256, .T. ) ;
#70310=LINE ( 'NONE', #62710, #77701 ) ;
#70321=FACE_OUTER_BOUND ( 'NONE', #16994, .T. ) ;
#70365=ORIENTED_EDGE ( 'NONE', *, *, #4451, .T. ) ;
#70433=CARTESIAN_POINT ( 'NONE',  ( 6.499999999999992895, -1.818455879622361558E-15, 4.499999999999999112 ) ) ;
#70488=PRODUCT_DEFINITION ( 'UNKNOWN', '', #11661, #4356 ) ;
#70494=CYLINDRICAL_SURFACE ( 'NONE', #50547, 1.250000000000001110 ) ;
#70568=DIRECTION ( 'NONE',  ( 0.000000000000000000, -0.000000000000000000, -1.000000000000000000 ) ) ;
#70600=DIRECTION ( 'NONE',  ( 0.000000000000000000, 0.000000000000000000, 1.000000000000000000 ) ) ;
#70675=DIRECTION ( 'NONE',  ( 0.9848077530122089085, 0.1736481776669261956, 0.000000000000000000 ) ) ;
#70682=ORIENTED_EDGE ( 'NONE', *, *, #2908, .T. ) ;
#70720=CYLINDRICAL_SURFACE ( 'NONE', #81732, 1.050000000000000488 ) ;
#70722=AXIS2_PLACEMENT_3D ( 'NONE', #28339, #74025, #82623 ) ;
#70744=DIRECTION ( 'NONE',  ( -0.000000000000000000, -0.000000000000000000, -1.000000000000000000 ) ) ;
#70766=VERTEX_POINT ( 'NONE', #18851 ) ;
#70843=CARTESIAN_POINT ( 'NONE',  ( -2.499999999999993339, 4.999999999999997335, 2.100000000000000089 ) ) ;
#70863=CIRCLE ( 'NONE', #93506, 1.000000000000000444 ) ;
#70866=CYLINDRICAL_SURFACE ( 'NONE', #88844, 1.000000000000000444 ) ;
#70901=ORIENTED_EDGE ( 'NONE', *, *, #61355, .F. ) ;
#70905=VERTEX_POINT ( 'NONE', #33969 ) ;
#70919=DIRECTION ( 'NONE',  ( -0.000000000000000000, -0.000000000000000000, -1.000000000000000000 ) ) ;
#70962=LINE ( 'NONE', #85171, #82630 ) ;
#70981=EDGE_CURVE ( 'NONE', #85384, #17017, #10634, .T. ) ;
#70987=EDGE_CURVE ( 'NONE', #75990, #57247, #73046, .T. ) ;
#70999=DIRECTION ( 'NONE',  ( 0.000000000000000000, -0.000000000000000000, -1.000000000000000000 ) ) ;
#71004=ORIENTED_EDGE ( 'NONE', *, *, #90712, .F. ) ;
#71036=EDGE_LOOP ( 'NONE', ( #43218, #17217, #91514, #21826 ) ) ;
#71060=EDGE_CURVE ( 'NONE', #10358, #80526, #44584, .T. ) ;
#71082=CARTESIAN_POINT ( 'NONE',  ( -10.34999999999999254, 4.999999999999999112, 2.100000000000000089 ) ) ;
#71131=VECTOR ( 'NONE', #72275, 1000.000000000000114 ) ;
#71356=DIRECTION ( 'NONE',  ( 0.000000000000000000, -0.000000000000000000, -1.000000000000000000 ) ) ;
#71373=FACE_OUTER_BOUND ( 'NONE', #56557, .T. ) ;
#71396=PLANE ( 'NONE',  #63277 ) ;
#71397=ORIENTED_EDGE ( 'NONE', *, *, #49348, .T. ) ;
#71415=EDGE_LOOP ( 'NONE', ( #68417, #1137, #16492, #60758 ) ) ;
#71445=ORIENTED_EDGE ( 'NONE', *, *, #55113, .F. ) ;
#71495=VECTOR ( 'NONE', #40532, 1000.000000000000000 ) ;
#71560=ORIENTED_EDGE ( 'NONE', *, *, #66413, .F. ) ;
#71562=CIRCLE ( 'NONE', #9980, 0.2499999999997798983 ) ;
#71604=FACE_OUTER_BOUND ( 'NONE', #99207, .T. ) ;
#71677=ORIENTED_EDGE ( 'NONE', *, *, #85922, .T. ) ;
#71682=PRODUCT ( 'Spring-loaded Plate_Varsay\X2\0131\X0\lan', 'Spring-loaded Plate_Varsay\X2\0131\X0\lan', '', ( #3230 ) ) ;
#71717=CIRCLE ( 'NONE', #52299, 1.050000000000000488 ) ;
#71860=DIRECTION ( 'NONE',  ( 0.000000000000000000, -0.000000000000000000, -1.000000000000000000 ) ) ;
#71929=EDGE_CURVE ( 'NONE', #64230, #50455, #23252, .T. ) ;
#71960=VECTOR ( 'NONE', #29273, 1000.000000000000000 ) ;
#72057=CARTESIAN_POINT ( 'NONE',  ( -8.376690734369036662, 11.49999999999999645, 2.100000000000000089 ) ) ;
#72096=DIRECTION ( 'NONE',  ( -1.000000000000000000, 0.000000000000000000, 0.000000000000000000 ) ) ;
#72102=DIRECTION ( 'NONE',  ( 1.000000000000000000, 3.389844910009033029E-15, 0.000000000000000000 ) ) ;
#72126=CIRCLE ( 'NONE', #760, 1.000000000000000444 ) ;
#72275=DIRECTION ( 'NONE',  ( 0.1736481776669262511, 0.9848077530122087975, 0.000000000000000000 ) ) ;
#72281=VERTEX_POINT ( 'NONE', #44999 ) ;
#72287=LINE ( 'NONE', #65690, #54304 ) ;
#72369=EDGE_CURVE ( 'NONE', #93232, #98936, #84041, .T. ) ;
#72416=CARTESIAN_POINT ( 'NONE',  ( 9.383883476483161346, 17.86611652351680846, 0.000000000000000000 ) ) ;
#72430=ORIENTED_EDGE ( 'NONE', *, *, #26862, .T. ) ;
#72434=ORIENTED_EDGE ( 'NONE', *, *, #3167, .T. ) ;
#72502=CARTESIAN_POINT ( 'NONE',  ( 3.737436867076077363, 13.63388347648318444, 0.000000000000000000 ) ) ;
#72531=FACE_OUTER_BOUND ( 'NONE', #23315, .T. ) ;
#72555=LINE ( 'NONE', #41612, #6999 ) ;
#72598=CARTESIAN_POINT ( 'NONE',  ( 2.499999999999995115, 19.99999999999999645, 2.100000000000000089 ) ) ;
#72628=EDGE_CURVE ( 'NONE', #62142, #23337, #91035, .T. ) ;
#72651=ORIENTED_EDGE ( 'NONE', *, *, #31004, .F. ) ;
#72719=LINE ( 'NONE', #3219, #92541 ) ;
#72742=ORIENTED_EDGE ( 'NONE', *, *, #90712, .T. ) ;
#72774=CARTESIAN_POINT ( 'NONE',  ( -2.899999999999996803, 31.80000000000000071, 2.100000000000000089 ) ) ;
#72800=LINE ( 'NONE', #25618, #37375 ) ;
#72808=PLANE ( 'NONE',  #36759 ) ;
#72830=DIRECTION ( 'NONE',  ( -1.000000000000000000, -4.476705744456278313E-16, 0.000000000000000000 ) ) ;
#72871=AXIS2_PLACEMENT_3D ( 'NONE', #80428, #57112, #74317 ) ;
#72916=ADVANCED_FACE ( 'NONE', ( #8803 ), #54478, .T. ) ;
#72990=ADVANCED_FACE ( 'NONE', ( #33644 ), #34647, .F. ) ;
#72991=EDGE_LOOP ( 'NONE', ( #85671, #43819, #87121, #59832, #69210, #1411, #56830, #25467, #57923, #92072, #80829, #76731, #80821, #38865, #23078, #34137, #40821, #22119, #79020, #61008, #10846, #85654, #81146, #26738, #97197, #24057, #71004, #17606, #3662, #72651, #63748, #9358, #32802, #97238, #83271, #5627, #69795, #50650, #16751, #26009, #93334, #76125, #62651, #46214, #30646, #27711 ) ) ;
#73030=VERTEX_POINT ( 'NONE', #75184 ) ;
#73046=LINE ( 'NONE', #43092, #76114 ) ;
#73119=LINE ( 'NONE', #80723, #93014 ) ;
#73121=DIRECTION ( 'NONE',  ( 1.000000000000000000, 0.000000000000000000, 0.000000000000000000 ) ) ;
#73146=CARTESIAN_POINT ( 'NONE',  ( 9.383883476483161346, 17.86611652351680846, 0.000000000000000000 ) ) ;
#73199=EDGE_CURVE ( 'NONE', #88129, #9489, #91406, .T. ) ;
#73228=CARTESIAN_POINT ( 'NONE',  ( -4.621320343559618848, 12.50000000000004974, 0.000000000000000000 ) ) ;
#73238=ORIENTED_EDGE ( 'NONE', *, *, #579, .F. ) ;
#73252=ORIENTED_EDGE ( 'NONE', *, *, #67527, .T. ) ;
#73290=ORIENTED_EDGE ( 'NONE', *, *, #18343, .F. ) ;
#73334=CARTESIAN_POINT ( 'NONE',  ( -6.499999999999992895, 3.983606557377048940, 3.319672131147540561 ) ) ;
#73380=VERTEX_POINT ( 'NONE', #26415 ) ;
#73455=LINE ( 'NONE', #89178, #915 ) ;
#73472=ORIENTED_EDGE ( 'NONE', *, *, #34884, .T. ) ;
#73499=ADVANCED_FACE ( 'NONE', ( #82187 ), #58374, .T. ) ;
#73510=DIRECTION ( 'NONE',  ( 0.7071067811865513475, 0.7071067811865435759, 0.000000000000000000 ) ) ;
#73536=ORIENTED_EDGE ( 'NONE', *, *, #65289, .T. ) ;
#73543=EDGE_CURVE ( 'NONE', #57983, #86, #27415, .T. ) ;
#73617=ORIENTED_EDGE ( 'NONE', *, *, #48878, .F. ) ;
#73710=VERTEX_POINT ( 'NONE', #7930 ) ;
#73735=DIRECTION ( 'NONE',  ( -0.000000000000000000, 1.000000000000000000, 1.084202172485504557E-16 ) ) ;
#73737=CARTESIAN_POINT ( 'NONE',  ( 2.499999999999994671, 18.99999999999977618, 2.100000000000000089 ) ) ;
#73743=EDGE_CURVE ( 'NONE', #75990, #32056, #62237, .T. ) ;
#73747=ORIENTED_EDGE ( 'NONE', *, *, #23061, .F. ) ;
#73794=DIRECTION ( 'NONE',  ( 1.000000000000000000, 0.000000000000000000, 0.000000000000000000 ) ) ;
#73824=DIRECTION ( 'NONE',  ( 0.000000000000000000, -0.000000000000000000, 1.000000000000000000 ) ) ;
#73851=EDGE_CURVE ( 'NONE', #76974, #38439, #90903, .T. ) ;
#73980=VERTEX_POINT ( 'NONE', #42900 ) ;
#74002=CARTESIAN_POINT ( 'NONE',  ( 3.750000000000001776, 26.59999999999999432, 0.000000000000000000 ) ) ;
#74003=LINE ( 'NONE', #59784, #88951 ) ;
#74025=DIRECTION ( 'NONE',  ( -0.000000000000000000, -0.000000000000000000, -1.000000000000000000 ) ) ;
#74087=ORIENTED_EDGE ( 'NONE', *, *, #93811, .T. ) ;
#74113=CARTESIAN_POINT ( 'NONE',  ( -10.34999999999997833, 22.00000000000000000, 2.100000000000000089 ) ) ;
#74158=CARTESIAN_POINT ( 'NONE',  ( 10.34999999999999254, 4.999999999999998224, 2.100000000000000089 ) ) ;
#74171=VERTEX_POINT ( 'NONE', #8314 ) ;
#74273=DIRECTION ( 'NONE',  ( 0.000000000000000000, -0.000000000000000000, -1.000000000000000000 ) ) ;
#74312=CARTESIAN_POINT ( 'NONE',  ( -6.499999999999992895, 1.000000000000000000, -2.500000000000001332 ) ) ;
#74317=DIRECTION ( 'NONE',  ( -1.000000000000000000, 0.000000000000000000, 0.000000000000000000 ) ) ;
#74322=EDGE_CURVE ( 'NONE', #53302, #37074, #53766, .T. ) ;
#74326=FACE_OUTER_BOUND ( 'NONE', #58696, .T. ) ;
#74362=CARTESIAN_POINT ( 'NONE',  ( 8.676776695296462449, 18.57322330470351091, 0.000000000000000000 ) ) ;
#74367=CARTESIAN_POINT ( 'NONE',  ( 4.621320343559255583, 11.49999999999999467, 2.100000000000000089 ) ) ;
#74388=ORIENTED_EDGE ( 'NONE', *, *, #11412, .F. ) ;
#74466=DIRECTION ( 'NONE',  ( -1.000000000000000000, 0.000000000000000000, 0.000000000000000000 ) ) ;
#74477=VECTOR ( 'NONE', #89521, 1000.000000000000000 ) ;
#74524=VECTOR ( 'NONE', #28069, 1000.000000000000000 ) ;
#74547=DIRECTION ( 'NONE',  ( 1.000000000000000000, -7.960204194457801640E-17, 0.000000000000000000 ) ) ;
#74551=CARTESIAN_POINT ( 'NONE',  ( 9.299999999999993605, 12.00000000000002309, 2.100000000000000089 ) ) ;
#74563=EDGE_CURVE ( 'NONE', #47721, #23558, #58503, .T. ) ;
#74660=ORIENTED_EDGE ( 'NONE', *, *, #86185, .T. ) ;
#74712=DIRECTION ( 'NONE',  ( -0.000000000000000000, -0.000000000000000000, -1.000000000000000000 ) ) ;
#74735=CARTESIAN_POINT ( 'NONE',  ( -6.499999999999993783, 3.000000000000000000, 4.499999999999999112 ) ) ;
#74741=CARTESIAN_POINT ( 'NONE',  ( 2.899999999999999467, 33.29999999999999716, 2.100000000000000089 ) ) ;
#74772=ORIENTED_EDGE ( 'NONE', *, *, #91833, .F. ) ;
#74989=ORIENTED_EDGE ( 'NONE', *, *, #62720, .T. ) ;
#75131=ORIENTED_EDGE ( 'NONE', *, *, #44913, .F. ) ;
#75184=CARTESIAN_POINT ( 'NONE',  ( -7.662324775236974972, 31.59999999999999787, 0.000000000000000000 ) ) ;
#75222=DIRECTION ( 'NONE',  ( -0.000000000000000000, -0.000000000000000000, -1.000000000000000000 ) ) ;
#75421=ORIENTED_EDGE ( 'NONE', *, *, #44913, .T. ) ;
#75442=ORIENTED_EDGE ( 'NONE', *, *, #48309, .T. ) ;
#75480=DIRECTION ( 'NONE',  ( -0.000000000000000000, -0.000000000000000000, -1.000000000000000000 ) ) ;
#75501=CARTESIAN_POINT ( 'NONE',  ( 7.749999999999998224, 23.99999999999999289, 2.100000000000000089 ) ) ;
#75526=VERTEX_POINT ( 'NONE', #25683 ) ;
#75550=FACE_OUTER_BOUND ( 'NONE', #48994, .T. ) ;
#75558=CIRCLE ( 'NONE', #70722, 1.050000000000000488 ) ;
#75604=ORIENTED_EDGE ( 'NONE', *, *, #37907, .T. ) ;
#75620=DIRECTION ( 'NONE',  ( 4.095491270384932624E-17, 0.5144957554275265688, -0.8574929257125440962 ) ) ;
#75639=ORIENTED_EDGE ( 'NONE', *, *, #46717, .T. ) ;
#75675=FACE_OUTER_BOUND ( 'NONE', #66547, .T. ) ;
#75694=ORIENTED_EDGE ( 'NONE', *, *, #65048, .T. ) ;
#75735=DIRECTION ( 'NONE',  ( 1.000000000000000000, 0.000000000000000000, 0.000000000000000000 ) ) ;
#75755=AXIS2_PLACEMENT_3D ( 'NONE', #91404, #96656, #6175 ) ;
#75759=ORIENTED_EDGE ( 'NONE', *, *, #80632, .F. ) ;
#75762=EDGE_CURVE ( 'NONE', #82244, #43107, #38108, .T. ) ;
#75862=VERTEX_POINT ( 'NONE', #16276 ) ;
#75870=EDGE_CURVE ( 'NONE', #89308, #27813, #2076, .T. ) ;
#75885=CARTESIAN_POINT ( 'NONE',  ( -8.349999999999971223, 27.69999999999999574, 0.000000000000000000 ) ) ;
#75900=LINE ( 'NONE', #69296, #21886 ) ;
#75948=DIRECTION ( 'NONE',  ( -1.000000000000000000, 0.000000000000000000, 0.000000000000000000 ) ) ;
#75989=ORIENTED_EDGE ( 'NONE', *, *, #16612, .F. ) ;
#75990=VERTEX_POINT ( 'NONE', #31499 ) ;
#76008=EDGE_CURVE ( 'NONE', #38439, #84685, #67846, .T. ) ;
#76101=CARTESIAN_POINT ( 'NONE',  ( 6.499999999999992895, 1.999999999999998668, 2.499999999999999112 ) ) ;
#76114=VECTOR ( 'NONE', #3532, 1000.000000000000000 ) ;
#76125=ORIENTED_EDGE ( 'NONE', *, *, #15843, .F. ) ;
#76190=LINE ( 'NONE', #68597, #17271 ) ;
#76250=ORIENTED_EDGE ( 'NONE', *, *, #17455, .T. ) ;
#76292=LINE ( 'NONE', #92521, #42695 ) ;
#76372=ADVANCED_FACE ( 'NONE', ( #1320 ), #24637, .T. ) ;
#76405=AXIS2_PLACEMENT_3D ( 'NONE', #77801, #39258, #70218 ) ;
#76689=DIRECTION ( 'NONE',  ( 0.000000000000000000, -0.000000000000000000, -1.000000000000000000 ) ) ;
#76731=ORIENTED_EDGE ( 'NONE', *, *, #86808, .F. ) ;
#76895=EDGE_CURVE ( 'NONE', #29229, #74171, #71717, .T. ) ;
#76926=LINE ( 'NONE', #8435, #32827 ) ;
#76951=FACE_OUTER_BOUND ( 'NONE', #87228, .T. ) ;
#76966=PLANE ( 'NONE',  #30162 ) ;
#76974=VERTEX_POINT ( 'NONE', #43641 ) ;
#76999=ORIENTED_EDGE ( 'NONE', *, *, #23879, .F. ) ;
#77128=DIRECTION ( 'NONE',  ( 0.000000000000000000, 0.000000000000000000, 1.000000000000000000 ) ) ;
#77213=AXIS2_PLACEMENT_3D ( 'NONE', #92501, #31604, #77760 ) ;
#77215=CARTESIAN_POINT ( 'NONE',  ( 10.34999999999998010, 22.00000000000000000, 2.100000000000000089 ) ) ;
#77224=DIRECTION ( 'NONE',  ( -3.469446951953611033E-15, -1.000000000000000000, 0.000000000000000000 ) ) ;
#77308=DIRECTION ( 'NONE',  ( 1.000000000000000000, 0.000000000000000000, 0.000000000000000000 ) ) ;
#77415=FACE_OUTER_BOUND ( 'NONE', #13219, .T. ) ;
#77426=DIRECTION ( 'NONE',  ( 1.000000000000000000, -2.209838822900391329E-16, 0.000000000000000000 ) ) ;
#77429=VECTOR ( 'NONE', #19851, 1000.000000000000000 ) ;
#77430=EDGE_CURVE ( 'NONE', #17712, #47723, #34912, .T. ) ;
#77476=CARTESIAN_POINT ( 'NONE',  ( 8.676776695296466002, 18.57322330470350735, 2.100000000000000089 ) ) ;
#77516=VECTOR ( 'NONE', #37832, 1000.000000000000000 ) ;
#77564=LINE ( 'NONE', #51374, #85025 ) ;
#77598=EDGE_CURVE ( 'NONE', #33368, #1165, #6952, .T. ) ;
#77602=DIRECTION ( 'NONE',  ( 0.000000000000000000, -0.000000000000000000, -1.000000000000000000 ) ) ;
#77644=AXIS2_PLACEMENT_3D ( 'NONE', #22311, #39054, #99441 ) ;
#77675=FACE_OUTER_BOUND ( 'NONE', #71036, .T. ) ;
#77701=VECTOR ( 'NONE', #85520, 1000.000000000000000 ) ;
#77760=DIRECTION ( 'NONE',  ( -1.000000000000000000, 0.000000000000000000, 0.000000000000000000 ) ) ;
#77801=CARTESIAN_POINT ( 'NONE',  ( -9.299999999999991829, 12.00000000000002309, 0.000000000000000000 ) ) ;
#77810=DIRECTION ( 'NONE',  ( 0.000000000000000000, -0.000000000000000000, -1.000000000000000000 ) ) ;
#77852=DIRECTION ( 'NONE',  ( -0.1736481776669262789, -0.9848077530122087975, 0.000000000000000000 ) ) ;
#77889=LINE ( 'NONE', #22600, #23784 ) ;
#78018=LINE ( 'NONE', #70433, #88057 ) ;
#78021=ORIENTED_EDGE ( 'NONE', *, *, #7531, .T. ) ;
#78078=DIRECTION ( 'NONE',  ( 0.7071067811865513475, -0.7071067811865437980, 0.000000000000000000 ) ) ;
#78276=EDGE_CURVE ( 'NONE', #88974, #40829, #86703, .T. ) ;
#78309=ORIENTED_EDGE ( 'NONE', *, *, #34640, .T. ) ;
#78352=ORIENTED_EDGE ( 'NONE', *, *, #42404, .F. ) ;
#78358=ORIENTED_EDGE ( 'NONE', *, *, #30522, .T. ) ;
#78377=CARTESIAN_POINT ( 'NONE',  ( 1.751198251822017937, 22.56127314141087581, 0.000000000000000000 ) ) ;
#78410=VECTOR ( 'NONE', #16461, 1000.000000000000114 ) ;
#78416=DIRECTION ( 'NONE',  ( 0.7071067811865437980, 0.7071067811865513475, -0.000000000000000000 ) ) ;
#78453=LINE ( 'NONE', #8956, #16708 ) ;
#78483=CARTESIAN_POINT ( 'NONE',  ( -2.899999999999996803, 33.29999999999999716, 2.100000000000000089 ) ) ;
#78492=ORIENTED_EDGE ( 'NONE', *, *, #59545, .T. ) ;
#78525=ORIENTED_EDGE ( 'NONE', *, *, #36387, .T. ) ;
#78559=DIRECTION ( 'NONE',  ( 0.000000000000000000, 0.000000000000000000, 1.000000000000000000 ) ) ;
#78735=AXIS2_PLACEMENT_3D ( 'NONE', #38753, #95930, #199 ) ;
#78745=DIRECTION ( 'NONE',  ( 1.000000000000000000, 0.000000000000000000, 0.000000000000000000 ) ) ;
#78853=CARTESIAN_POINT ( 'NONE',  ( -4.621320343559618848, 12.50000000000004974, 2.100000000000000089 ) ) ;
#78884=AXIS2_PLACEMENT_3D ( 'NONE', #69507, #61903, #54295 ) ;
#78923=DIRECTION ( 'NONE',  ( 0.000000000000000000, 0.000000000000000000, 1.000000000000000000 ) ) ;
#78939=CARTESIAN_POINT ( 'NONE',  ( -10.34999999999999254, -1.301042606982604926E-15, 4.499999999999999112 ) ) ;
#79016=ORIENTED_EDGE ( 'NONE', *, *, #11412, .T. ) ;
#79020=ORIENTED_EDGE ( 'NONE', *, *, #30701, .T. ) ;
#79103=DIRECTION ( 'NONE',  ( 0.000000000000000000, 0.000000000000000000, 1.000000000000000000 ) ) ;
#79148=EDGE_CURVE ( 'NONE', #86751, #82984, #35135, .T. ) ;
#79218=DIRECTION ( 'NONE',  ( 1.000000000000000000, -7.960204194457801640E-17, 0.000000000000000000 ) ) ;
#79246=VERTEX_POINT ( 'NONE', #80301 ) ;
#79285=CARTESIAN_POINT ( 'NONE',  ( 7.749999999999998224, 25.69999999999999574, 2.100000000000000089 ) ) ;
#79328=PLANE ( 'NONE',  #82977 ) ;
#79364=DIRECTION ( 'NONE',  ( -1.000000000000000000, 0.000000000000000000, 0.000000000000000000 ) ) ;
#79374=DIRECTION ( 'NONE',  ( 1.000000000000000000, -7.960204194457801640E-17, 0.000000000000000000 ) ) ;
#79375=CARTESIAN_POINT ( 'NONE',  ( -8.499999999999987566, 18.74999999999999645, 0.000000000000000000 ) ) ;
#79541=EDGE_LOOP ( 'NONE', ( #23998, #34271, #31172, #26255 ) ) ;
#79607=DIRECTION ( 'NONE',  ( 1.000000000000000000, 0.000000000000000000, 0.000000000000000000 ) ) ;
#79625=DIRECTION ( 'NONE',  ( -1.000000000000000000, 3.469446951953611033E-15, 0.000000000000000000 ) ) ;
#79628=ORIENTED_EDGE ( 'NONE', *, *, #70981, .T. ) ;
#79669=ADVANCED_FACE ( 'NONE', ( #65713 ), #59085, .F. ) ;
#79688=CARTESIAN_POINT ( 'NONE',  ( -3.737436867076076030, 13.63388347648318444, 0.000000000000000000 ) ) ;
#79693=EDGE_CURVE ( 'NONE', #57281, #33604, #43852, .T. ) ;
#79754=CARTESIAN_POINT ( 'NONE',  ( 8.749999999999769074, 18.74999999999999645, 2.100000000000000089 ) ) ;
#79756=DIRECTION ( 'NONE',  ( -0.7071067811865434649, 0.7071067811865516806, 0.000000000000000000 ) ) ;
#79852=VECTOR ( 'NONE', #41108, 1000.000000000000000 ) ;
#79926=ADVANCED_FACE ( 'NONE', ( #54959 ), #2182, .T. ) ;
#79930=CIRCLE ( 'NONE', #13435, 1.249999999999997558 ) ;
#80132=CARTESIAN_POINT ( 'NONE',  ( -9.749999999999984013, 18.74999999999999645, 0.000000000000000000 ) ) ;
#80159=DIRECTION ( 'NONE',  ( 0.000000000000000000, 0.000000000000000000, 1.000000000000000000 ) ) ;
#80164=ORIENTED_EDGE ( 'NONE', *, *, #26253, .F. ) ;
#80186=LINE ( 'NONE', #87802, #22216 ) ;
#80214=VECTOR ( 'NONE', #84583, 1000.000000000000000 ) ;
#80254=VERTEX_POINT ( 'NONE', #87278 ) ;
#80267=EDGE_LOOP ( 'NONE', ( #81164, #78352, #28295, #78525, #85127, #57086 ) ) ;
#80271=CARTESIAN_POINT ( 'NONE',  ( -2.749999999999999112, 26.59999999999999432, 0.000000000000000000 ) ) ;
#80301=CARTESIAN_POINT ( 'NONE',  ( -8.499999999999987566, 18.99999999999977973, 0.000000000000000000 ) ) ;
#80333=APPLICATION_CONTEXT ( 'configuration controlled 3d designs of mechanical parts and assemblies' ) ;
#80340=CARTESIAN_POINT ( 'NONE',  ( 8.599999999999999645, 24.84999999999999787, 0.000000000000000000 ) ) ;
#80352=CIRCLE ( 'NONE', #8360, 1.050000000000000488 ) ;
#80389=VERTEX_POINT ( 'NONE', #10665 ) ;
#80397=CARTESIAN_POINT ( 'NONE',  ( 10.34999999999998010, 27.69999999999999929, 0.000000000000000000 ) ) ;
#80427=CIRCLE ( 'NONE', #5892, 1.250000000000001998 ) ;
#80428=CARTESIAN_POINT ( 'NONE',  ( -4.621320343559624177, 12.75000000000004974, 2.100000000000000089 ) ) ;
#80435=VECTOR ( 'NONE', #55996, 1000.000000000000000 ) ;
#80441=AXIS2_PLACEMENT_3D ( 'NONE', #93187, #93689, #86582 ) ;
#80465=VECTOR ( 'NONE', #83500, 1000.000000000000000 ) ;
#80526=VERTEX_POINT ( 'NONE', #67956 ) ;
#80585=EDGE_CURVE ( 'NONE', #82122, #15222, #23754, .T. ) ;
#80621=ORIENTED_EDGE ( 'NONE', *, *, #65289, .F. ) ;
#80632=EDGE_CURVE ( 'NONE', #61087, #8902, #12899, .T. ) ;
#80638=FACE_OUTER_BOUND ( 'NONE', #3150, .T. ) ;
#80649=VECTOR ( 'NONE', #47240, 1000.000000000000000 ) ;
#80660=VERTEX_POINT ( 'NONE', #98631 ) ;
#80713=CARTESIAN_POINT ( 'NONE',  ( -4.444543648262984981, 12.92677669529668627, 0.000000000000000000 ) ) ;
#80723=CARTESIAN_POINT ( 'NONE',  ( -8.676776695296460673, 18.57322330470351091, 2.100000000000000089 ) ) ;
#80737=DIRECTION ( 'NONE',  ( 0.000000000000000000, 4.336808689942019708E-16, -1.000000000000000000 ) ) ;
#80821=ORIENTED_EDGE ( 'NONE', *, *, #46551, .F. ) ;
#80829=ORIENTED_EDGE ( 'NONE', *, *, #26862, .F. ) ;
#80885=DIRECTION ( 'NONE',  ( -0.000000000000000000, -0.000000000000000000, -1.000000000000000000 ) ) ;
#80889=DIRECTION ( 'NONE',  ( -1.000000000000000000, 0.000000000000000000, 0.000000000000000000 ) ) ;
#80910=CARTESIAN_POINT ( 'NONE',  ( -2.749999999999999112, 27.59999999999999432, 2.100000000000000089 ) ) ;
#81041=ORIENTED_EDGE ( 'NONE', *, *, #14930, .T. ) ;
#81072=CARTESIAN_POINT ( 'NONE',  ( -2.499999999999993339, 19.99999999999999645, 0.000000000000000000 ) ) ;
#81117=CARTESIAN_POINT ( 'NONE',  ( 9.383883476483161346, 17.86611652351680846, 2.100000000000000089 ) ) ;
#81144=EDGE_LOOP ( 'NONE', ( #1911, #73617, #91244, #29147, #74388, #75759, #56156, #11623, #22343 ) ) ;
#81146=ORIENTED_EDGE ( 'NONE', *, *, #16612, .T. ) ;
#81164=ORIENTED_EDGE ( 'NONE', *, *, #34640, .F. ) ;
#81197=DIRECTION ( 'NONE',  ( 0.000000000000000000, -0.000000000000000000, -1.000000000000000000 ) ) ;
#81234=EDGE_CURVE ( 'NONE', #69616, #53302, #98805, .T. ) ;
#81264=EDGE_CURVE ( 'NONE', #73710, #59693, #52851, .T. ) ;
#81280=FACE_OUTER_BOUND ( 'NONE', #14452, .T. ) ;
#81374=CARTESIAN_POINT ( 'NONE',  ( -7.749999999999996447, 24.84999999999999787, 2.100000000000000089 ) ) ;
#81402=VECTOR ( 'NONE', #95077, 1000.000000000000000 ) ;
#81432=DIRECTION ( 'NONE',  ( -7.960204194457801640E-17, -1.000000000000000000, -4.336808689942018722E-16 ) ) ;
#81435=FACE_OUTER_BOUND ( 'NONE', #15000, .T. ) ;
#81517=DIRECTION ( 'NONE',  ( 1.000000000000000000, -2.209838822900391329E-16, 0.000000000000000000 ) ) ;
#81553=CIRCLE ( 'NONE', #31344, 0.2500000000000011102 ) ;
#81639=PLANE ( 'NONE',  #11169 ) ;
#81679=LINE ( 'NONE', #52726, #42190 ) ;
#81721=DIRECTION ( 'NONE',  ( 0.000000000000000000, -0.000000000000000000, -1.000000000000000000 ) ) ;
#81723=LINE ( 'NONE', #74113, #4131 ) ;
#81726=ORIENTED_EDGE ( 'NONE', *, *, #48405, .F. ) ;
#81732=AXIS2_PLACEMENT_3D ( 'NONE', #24537, #55506, #64137 ) ;
#81738=EDGE_CURVE ( 'NONE', #24018, #85384, #54249, .T. ) ;
#81792=ORIENTED_EDGE ( 'NONE', *, *, #40624, .F. ) ;
#81866=DIRECTION ( 'NONE',  ( -1.000000000000000000, 0.000000000000000000, 0.000000000000000000 ) ) ;
#82108=DIRECTION ( 'NONE',  ( 0.000000000000000000, 0.000000000000000000, 1.000000000000000000 ) ) ;
#82122=VERTEX_POINT ( 'NONE', #81072 ) ;
#82136=AXIS2_PLACEMENT_3D ( 'NONE', #93136, #41881, #32747 ) ;
#82187=FACE_OUTER_BOUND ( 'NONE', #59444, .T. ) ;
#82244=VERTEX_POINT ( 'NONE', #92657 ) ;
#82263=VECTOR ( 'NONE', #96141, 1000.000000000000000 ) ;
#82275=FACE_OUTER_BOUND ( 'NONE', #80267, .T. ) ;
#82292=ORIENTED_EDGE ( 'NONE', *, *, #77598, .F. ) ;
#82306=CIRCLE ( 'NONE', #98441, 0.2499999999997798983 ) ;
#82351=CIRCLE ( 'NONE', #48403, 0.2499999999997798983 ) ;
#82419=CARTESIAN_POINT ( 'NONE',  ( -10.34999999999999254, 0.000000000000000000, -2.500000000000001332 ) ) ;
#82425=ORIENTED_EDGE ( 'NONE', *, *, #85922, .F. ) ;
#82428=DIRECTION ( 'NONE',  ( -0.000000000000000000, -0.000000000000000000, -1.000000000000000000 ) ) ;
#82504=DIRECTION ( 'NONE',  ( 0.1736481776669262511, 0.9848077530122087975, 0.000000000000000000 ) ) ;
#82508=DIRECTION ( 'NONE',  ( 0.000000000000000000, -0.8574929257125442073, -0.5144957554275266798 ) ) ;
#82515=DIRECTION ( 'NONE',  ( -7.960204194457801640E-17, -1.000000000000000000, 1.571307496355802463E-16 ) ) ;
#82591=ORIENTED_EDGE ( 'NONE', *, *, #80632, .T. ) ;
#82607=DIRECTION ( 'NONE',  ( 0.000000000000000000, -0.000000000000000000, -1.000000000000000000 ) ) ;
#82615=ORIENTED_EDGE ( 'NONE', *, *, #48517, .T. ) ;
#82623=DIRECTION ( 'NONE',  ( -1.000000000000000000, 0.000000000000000000, 0.000000000000000000 ) ) ;
#82630=VECTOR ( 'NONE', #63367, 1000.000000000000000 ) ;
#82793=CARTESIAN_POINT ( 'NONE',  ( 4.444543648262985869, 12.92677669529668627, 2.100000000000000089 ) ) ;
#82801=ORIENTED_EDGE ( 'NONE', *, *, #83686, .T. ) ;
#82844=CARTESIAN_POINT ( 'NONE',  ( -2.499999999999993339, 18.99999999999977618, 2.100000000000000089 ) ) ;
#82848=AXIS2_PLACEMENT_3D ( 'NONE', #36014, #90806, #96424 ) ;
#82891=LINE ( 'NONE', #5277, #44986 ) ;
#82977=AXIS2_PLACEMENT_3D ( 'NONE', #69732, #16421, #77810 ) ;
#82984=VERTEX_POINT ( 'NONE', #5575 ) ;
#83010=ORIENTED_EDGE ( 'NONE', *, *, #24268, .F. ) ;
#83020=DIRECTION ( 'NONE',  ( -1.000000000000000000, 0.000000000000000000, 0.000000000000000000 ) ) ;
#83105=ORIENTED_EDGE ( 'NONE', *, *, #84463, .F. ) ;
#83169=DIRECTION ( 'NONE',  ( 0.000000000000000000, -0.000000000000000000, -1.000000000000000000 ) ) ;
#83271=ORIENTED_EDGE ( 'NONE', *, *, #91344, .T. ) ;
#83300=VERTEX_POINT ( 'NONE', #93388 ) ;
#83310=SHAPE_DEFINITION_REPRESENTATION ( #56309, #50921 ) ;
#83351=CARTESIAN_POINT ( 'NONE',  ( -3.749999999999999112, 25.69999999999999574, 2.100000000000000089 ) ) ;
#83381=EDGE_CURVE ( 'NONE', #17782, #73380, #1566, .T. ) ;
#83426=VECTOR ( 'NONE', #71860, 1000.000000000000000 ) ;
#83500=DIRECTION ( 'NONE',  ( 1.000000000000000000, 0.000000000000000000, 0.000000000000000000 ) ) ;
#83538=AXIS2_PLACEMENT_3D ( 'NONE', #52736, #14663, #38507 ) ;
#83619=FACE_OUTER_BOUND ( 'NONE', #66706, .T. ) ;
#83671=FACE_OUTER_BOUND ( 'NONE', #14961, .T. ) ;
#83686=EDGE_CURVE ( 'NONE', #29751, #80660, #86169, .T. ) ;
#83689=LINE ( 'NONE', #454, #91964 ) ;
#83719=CARTESIAN_POINT ( 'NONE',  ( -1.751198251822016161, 22.56127314141087581, 2.100000000000000089 ) ) ;
#83801=EDGE_CURVE ( 'NONE', #82984, #57281, #70863, .T. ) ;
#83859=EDGE_LOOP ( 'NONE', ( #26146, #31730, #79628, #34816, #31837, #31727, #34381, #13947, #68889 ) ) ;
#84041=LINE ( 'NONE', #37871, #87662 ) ;
#84056=LINE ( 'NONE', #99276, #71960 ) ;
#84099=CYLINDRICAL_SURFACE ( 'NONE', #49735, 1.249999999999997558 ) ;
#84125=EDGE_LOOP ( 'NONE', ( #36207, #5879, #55368, #5891 ) ) ;
#84132=ORIENTED_EDGE ( 'NONE', *, *, #81234, .F. ) ;
#84172=DIRECTION ( 'NONE',  ( 0.000000000000000000, -1.000000000000000000, 0.000000000000000000 ) ) ;
#84196=ADVANCED_FACE ( 'NONE', ( #77415 ), #810, .F. ) ;
#84225=DIRECTION ( 'NONE',  ( 1.000000000000000000, 0.000000000000000000, 0.000000000000000000 ) ) ;
#84226=EDGE_CURVE ( 'NONE', #5121, #88129, #37877, .T. ) ;
#84244=ORIENTED_EDGE ( 'NONE', *, *, #31572, .F. ) ;
#84405=ADVANCED_FACE ( 'NONE', ( #75675 ), #65737, .T. ) ;
#84463=EDGE_CURVE ( 'NONE', #68021, #87155, #564, .T. ) ;
#84535=DIRECTION ( 'NONE',  ( -0.7071067811865513475, 0.7071067811865437980, 0.000000000000000000 ) ) ;
#84554=CIRCLE ( 'NONE', #22964, 1.050000000000000488 ) ;
#84570=FACE_OUTER_BOUND ( 'NONE', #44059, .T. ) ;
#84583=DIRECTION ( 'NONE',  ( -7.960204194457801640E-17, -1.000000000000000000, 0.000000000000000000 ) ) ;
#84666=DIRECTION ( 'NONE',  ( 1.000000000000000000, -7.960204194457801640E-17, 0.000000000000000000 ) ) ;
#84685=VERTEX_POINT ( 'NONE', #79688 ) ;
#84731=ORIENTED_EDGE ( 'NONE', *, *, #31497, .T. ) ;
#84798=CARTESIAN_POINT ( 'NONE',  ( 10.34999999999998010, 27.69999999999999929, 0.000000000000000000 ) ) ;
#84910=EDGE_CURVE ( 'NONE', #69181, #5121, #55255, .T. ) ;
#84964=ORIENTED_EDGE ( 'NONE', *, *, #32810, .T. ) ;
#85025=VECTOR ( 'NONE', #30903, 1000.000000000000000 ) ;
#85082=SHAPE_REPRESENTATION_RELATIONSHIP ( 'NONE' , 'NONE' ,  #50921, #12552 ) ;
#85127=ORIENTED_EDGE ( 'NONE', *, *, #60505, .T. ) ;
#85131=CARTESIAN_POINT ( 'NONE',  ( -10.34999999999999254, 3.851859888774471706E-31, 4.499999999999999112 ) ) ;
#85152=CARTESIAN_POINT ( 'NONE',  ( 6.499999999999992895, 0.9999999999999988898, 3.499999999999998668 ) ) ;
#85171=CARTESIAN_POINT ( 'NONE',  ( 6.499999999999992895, -5.174132726397565334E-16, -2.500000000000001332 ) ) ;
#85200=VECTOR ( 'NONE', #79364, 1000.000000000000000 ) ;
#85206=AXIS2_PLACEMENT_3D ( 'NONE', #1927, #48102, #65351 ) ;
#85214=CARTESIAN_POINT ( 'NONE',  ( 8.499999999999989342, 18.99999999999977973, 2.100000000000000089 ) ) ;
#85226=CARTESIAN_POINT ( 'NONE',  ( 8.499999999999989342, 19.99999999999999289, 2.100000000000000089 ) ) ;
#85238=ORIENTED_EDGE ( 'NONE', *, *, #90665, .F. ) ;
#85245=VERTEX_POINT ( 'NONE', #46013 ) ;
#85266=VECTOR ( 'NONE', #34583, 1000.000000000000114 ) ;
#85310=ORIENTED_EDGE ( 'NONE', *, *, #15294, .F. ) ;
#85331=AXIS2_PLACEMENT_3D ( 'NONE', #66542, #80737, #26945 ) ;
#85378=ORIENTED_EDGE ( 'NONE', *, *, #34893, .T. ) ;
#85384=VERTEX_POINT ( 'NONE', #11440 ) ;
#85392=ADVANCED_FACE ( 'NONE', ( #57632 ), #64766, .T. ) ;
#85425=DIRECTION ( 'NONE',  ( 0.000000000000000000, -0.000000000000000000, -1.000000000000000000 ) ) ;
#85476=PLANE ( 'NONE',  #12251 ) ;
#85519=ORIENTED_EDGE ( 'NONE', *, *, #24937, .F. ) ;
#85520=DIRECTION ( 'NONE',  ( -0.000000000000000000, -0.000000000000000000, -1.000000000000000000 ) ) ;
#85587=DIRECTION ( 'NONE',  ( -1.413818403454611288E-16, 1.000000000000000000, 0.000000000000000000 ) ) ;
#85610=EDGE_LOOP ( 'NONE', ( #35731, #75442, #58355, #60077 ) ) ;
#85654=ORIENTED_EDGE ( 'NONE', *, *, #69583, .T. ) ;
#85660=DIRECTION ( 'NONE',  ( 1.000000000000000000, 0.000000000000000000, 0.000000000000000000 ) ) ;
#85671=ORIENTED_EDGE ( 'NONE', *, *, #63082, .T. ) ;
#85706=VECTOR ( 'NONE', #44425, 1000.000000000000000 ) ;
#85757=VERTEX_POINT ( 'NONE', #22521 ) ;
#85922=EDGE_CURVE ( 'NONE', #75526, #41954, #30495, .T. ) ;
#86070=CARTESIAN_POINT ( 'NONE',  ( -6.499999999999992895, 1.999999999999999112, 0.000000000000000000 ) ) ;
#86105=EDGE_CURVE ( 'NONE', #50455, #69616, #42299, .T. ) ;
#86169=LINE ( 'NONE', #61351, #69182 ) ;
#86185=EDGE_CURVE ( 'NONE', #33250, #32160, #53384, .T. ) ;
#86202=VECTOR ( 'NONE', #36617, 1000.000000000000000 ) ;
#86249=VECTOR ( 'NONE', #48675, 1000.000000000000000 ) ;
#86290=DIRECTION ( 'NONE',  ( 0.000000000000000000, 1.084202172485504434E-16, -1.000000000000000000 ) ) ;
#86366=ORIENTED_EDGE ( 'NONE', *, *, #74322, .T. ) ;
#86421=EDGE_CURVE ( 'NONE', #55779, #20587, #82351, .T. ) ;
#86508=CARTESIAN_POINT ( 'NONE',  ( -3.749999999999999556, 26.59999999999999432, 2.100000000000000089 ) ) ;
#86520=CARTESIAN_POINT ( 'NONE',  ( 8.349999999999972999, 27.69999999999999574, 2.100000000000000089 ) ) ;
#86545=EDGE_CURVE ( 'NONE', #66209, #72281, #90197, .T. ) ;
#86546=DIRECTION ( 'NONE',  ( -1.000000000000000000, 0.000000000000000000, 0.000000000000000000 ) ) ;
#86568=CARTESIAN_POINT ( 'NONE',  ( -8.749999999999767297, 18.74999999999999645, 2.100000000000000089 ) ) ;
#86582=DIRECTION ( 'NONE',  ( -1.000000000000000000, 0.000000000000000000, 0.000000000000000000 ) ) ;
#86618=ORIENTED_EDGE ( 'NONE', *, *, #5340, .F. ) ;
#86703=LINE ( 'NONE', #17193, #11874 ) ;
#86719=CARTESIAN_POINT ( 'NONE',  ( -7.749999999999996447, 24.84999999999999787, 2.100000000000000089 ) ) ;
#86751=VERTEX_POINT ( 'NONE', #88095 ) ;
#86808=EDGE_CURVE ( 'NONE', #57983, #91978, #100146, .T. ) ;
#86809=CARTESIAN_POINT ( 'NONE',  ( -9.299999999999991829, 12.00000000000002309, 2.100000000000000089 ) ) ;
#86830=ORIENTED_EDGE ( 'NONE', *, *, #83801, .T. ) ;
#86904=VECTOR ( 'NONE', #20282, 1000.000000000000000 ) ;
#86912=CARTESIAN_POINT ( 'NONE',  ( 6.499999999999992895, 2.239999999999996660, 2.100000000000000977 ) ) ;
#86920=DIRECTION ( 'NONE',  ( -1.000000000000000000, 0.000000000000000000, 0.000000000000000000 ) ) ;
#86971=DIRECTION ( 'NONE',  ( -0.000000000000000000, -0.000000000000000000, -1.000000000000000000 ) ) ;
#87069=CARTESIAN_POINT ( 'NONE',  ( -6.499999999999992895, 3.299745742347187193E-16, 2.100000000000000977 ) ) ;
#87121=ORIENTED_EDGE ( 'NONE', *, *, #23191, .T. ) ;
#87152=AXIS2_PLACEMENT_3D ( 'NONE', #33149, #59494, #90932 ) ;
#87155=VERTEX_POINT ( 'NONE', #2236 ) ;
#87228=EDGE_LOOP ( 'NONE', ( #17982, #88625, #18691, #61940 ) ) ;
#87244=ORIENTED_EDGE ( 'NONE', *, *, #1557, .T. ) ;
#87253=ORIENTED_EDGE ( 'NONE', *, *, #97852, .T. ) ;
#87270=ORIENTED_EDGE ( 'NONE', *, *, #27562, .F. ) ;
#87278=CARTESIAN_POINT ( 'NONE',  ( -8.599999999999997868, 24.84999999999999787, 2.100000000000000089 ) ) ;
#87357=ADVANCED_FACE ( 'NONE', ( #80638 ), #81639, .F. ) ;
#87391=CARTESIAN_POINT ( 'NONE',  ( -4.621320343559254695, 11.49999999999999467, 2.100000000000000089 ) ) ;
#87487=LINE ( 'NONE', #17472, #47022 ) ;
#87517=EDGE_LOOP ( 'NONE', ( #15265, #90142, #56322, #66734 ) ) ;
#87582=EDGE_CURVE ( 'NONE', #90981, #88018, #392, .T. ) ;
#87662=VECTOR ( 'NONE', #35877, 1000.000000000000000 ) ;
#87697=DIRECTION ( 'NONE',  ( 7.960204194457801640E-17, 1.000000000000000000, -0.000000000000000000 ) ) ;
#87776=DIRECTION ( 'NONE',  ( 0.000000000000000000, -0.000000000000000000, -1.000000000000000000 ) ) ;
#87802=CARTESIAN_POINT ( 'NONE',  ( 8.376690734369038438, 11.49999999999999645, 2.100000000000000089 ) ) ;
#87805=CARTESIAN_POINT ( 'NONE',  ( 2.899999999999999467, 31.80000000000000071, 0.000000000000000000 ) ) ;
#87832=ADVANCED_FACE ( 'NONE', ( #61197 ), #14490, .T. ) ;
#87858=ORIENTED_EDGE ( 'NONE', *, *, #71060, .T. ) ;
#88002=CARTESIAN_POINT ( 'NONE',  ( 8.499999999999989342, 18.74999999999999645, 0.000000000000000000 ) ) ;
#88018=VERTEX_POINT ( 'NONE', #24099 ) ;
#88029=DIRECTION ( 'NONE',  ( -0.000000000000000000, 0.000000000000000000, -1.000000000000000000 ) ) ;
#88048=LINE ( 'NONE', #55603, #95094 ) ;
#88057=VECTOR ( 'NONE', #62841, 1000.000000000000000 ) ;
#88077=DIRECTION ( 'NONE',  ( -1.000000000000000000, 0.000000000000000000, 0.000000000000000000 ) ) ;
#88095=CARTESIAN_POINT ( 'NONE',  ( -3.749999999999999112, 25.69999999999999574, 2.100000000000000089 ) ) ;
#88129=VERTEX_POINT ( 'NONE', #80397 ) ;
#88169=DIRECTION ( 'NONE',  ( 1.734723475976801178E-15, 1.000000000000000000, -0.000000000000000000 ) ) ;
#88324=CARTESIAN_POINT ( 'NONE',  ( -2.899999999999996803, 31.80000000000000071, 0.000000000000000000 ) ) ;
#88342=VECTOR ( 'NONE', #99234, 1000.000000000000000 ) ;
#88398=VECTOR ( 'NONE', #4343, 1000.000000000000000 ) ;
#88408=VECTOR ( 'NONE', #83169, 1000.000000000000000 ) ;
#88425=DIRECTION ( 'NONE',  ( 1.000000000000000000, -7.960204194457801640E-17, -0.000000000000000000 ) ) ;
#88541=ORIENTED_EDGE ( 'NONE', *, *, #81264, .F. ) ;
#88584=DIRECTION ( 'NONE',  ( 1.000000000000000000, 1.224646799147353207E-16, 0.000000000000000000 ) ) ;
#88586=AXIS2_PLACEMENT_3D ( 'NONE', #52567, #6387, #60689 ) ;
#88625=ORIENTED_EDGE ( 'NONE', *, *, #42071, .F. ) ;
#88770=AXIS2_PLACEMENT_3D ( 'NONE', #69455, #84172, #45132 ) ;
#88801=EDGE_LOOP ( 'NONE', ( #66911, #41983, #72742, #9270 ) ) ;
#88844=AXIS2_PLACEMENT_3D ( 'NONE', #1356, #92678, #31797 ) ;
#88869=CARTESIAN_POINT ( 'NONE',  ( 6.499999999999993783, 2.999999999999999556, 4.499999999999999112 ) ) ;
#88902=EDGE_CURVE ( 'NONE', #79246, #76974, #38745, .T. ) ;
#88925=DIRECTION ( 'NONE',  ( 1.000000000000000000, 0.000000000000000000, 0.000000000000000000 ) ) ;
#88951=VECTOR ( 'NONE', #12591, 1000.000000000000000 ) ;
#88952=ADVANCED_FACE ( 'NONE', ( #94376 ), #17252, .T. ) ;
#88970=AXIS2_PLACEMENT_3D ( 'NONE', #60769, #29302, #91199 ) ;
#88974=VERTEX_POINT ( 'NONE', #65464 ) ;
#89024=ORIENTED_EDGE ( 'NONE', *, *, #49348, .F. ) ;
#89037=ORIENTED_EDGE ( 'NONE', *, *, #39707, .F. ) ;
#89103=CYLINDRICAL_SURFACE ( 'NONE', #20917, 1.249999999999997558 ) ;
#89115=VECTOR ( 'NONE', #81432, 1000.000000000000000 ) ;
#89178=CARTESIAN_POINT ( 'NONE',  ( -10.34999999999997833, 27.69999999999999929, 2.100000000000000089 ) ) ;
#89239=ORIENTED_EDGE ( 'NONE', *, *, #2617, .F. ) ;
#89256=ORIENTED_EDGE ( 'NONE', *, *, #93522, .T. ) ;
#89274=ORIENTED_EDGE ( 'NONE', *, *, #86421, .T. ) ;
#89296=EDGE_CURVE ( 'NONE', #34878, #40829, #70310, .T. ) ;
#89308=VERTEX_POINT ( 'NONE', #67942 ) ;
#89313=PLANE ( 'NONE',  #35034 ) ;
#89314=EDGE_CURVE ( 'NONE', #72281, #68666, #24121, .T. ) ;
#89318=CARTESIAN_POINT ( 'NONE',  ( -10.34999999999999254, 3.000000000000000000, 4.499999999999999112 ) ) ;
#89333=VERTEX_POINT ( 'NONE', #1301 ) ;
#89380=LINE ( 'NONE', #11748, #77429 ) ;
#89499=CARTESIAN_POINT ( 'NONE',  ( 8.376690734369038438, 12.50000000000004974, 2.100000000000000089 ) ) ;
#89521=DIRECTION ( 'NONE',  ( 1.000000000000000000, 0.000000000000000000, 0.000000000000000000 ) ) ;
#89548=AXIS2_PLACEMENT_3D ( 'NONE', #35614, #3176, #11759 ) ;
#89651=CARTESIAN_POINT ( 'NONE',  ( 9.299999999999993605, 12.00000000000002309, 0.000000000000000000 ) ) ;
#89681=CARTESIAN_POINT ( 'NONE',  ( 8.376690734369038438, 11.49999999999999645, 0.000000000000000000 ) ) ;
#89812=CARTESIAN_POINT ( 'NONE',  ( 4.621320343559619737, 12.50000000000004974, 0.000000000000000000 ) ) ;
#89844=DIRECTION ( 'NONE',  ( 0.000000000000000000, 1.000000000000000000, 0.000000000000000000 ) ) ;
#89892=ORIENTED_EDGE ( 'NONE', *, *, #21172, .T. ) ;
#89937=ORIENTED_EDGE ( 'NONE', *, *, #29950, .F. ) ;
#89946=DIRECTION ( 'NONE',  ( -1.000000000000000000, 0.000000000000000000, 0.000000000000000000 ) ) ;
#89981=VECTOR ( 'NONE', #93711, 1000.000000000000114 ) ;
#90037=VECTOR ( 'NONE', #30550, 1000.000000000000000 ) ;
#90039=DIRECTION ( 'NONE',  ( 0.000000000000000000, 1.000000000000000000, 0.000000000000000000 ) ) ;
#90044=PLANE ( 'NONE',  #61974 ) ;
#90137=ORIENTED_EDGE ( 'NONE', *, *, #47879, .F. ) ;
#90142=ORIENTED_EDGE ( 'NONE', *, *, #93784, .F. ) ;
#90184=CARTESIAN_POINT ( 'NONE',  ( 4.444543648262985869, 12.92677669529668627, 0.000000000000000000 ) ) ;
#90191=FACE_BOUND ( 'NONE', #24106, .T. ) ;
#90197=LINE ( 'NONE', #20178, #14324 ) ;
#90223=EDGE_CURVE ( 'NONE', #14365, #61087, #81679, .T. ) ;
#90297=DIRECTION ( 'NONE',  ( 1.000000000000000000, -7.960204194457801640E-17, 0.000000000000000000 ) ) ;
#90323=ORIENTED_EDGE ( 'NONE', *, *, #63603, .F. ) ;
#90345=ORIENTED_EDGE ( 'NONE', *, *, #15917, .F. ) ;
#90384=DIRECTION ( 'NONE',  ( -1.000000000000000000, 0.000000000000000000, 0.000000000000000000 ) ) ;
#90442=CARTESIAN_POINT ( 'NONE',  ( -3.737436867076076030, 13.63388347648318444, 2.100000000000000089 ) ) ;
#90541=CARTESIAN_POINT ( 'NONE',  ( -4.621320343559261801, 12.74999999999999645, 2.100000000000000089 ) ) ;
#90591=FACE_OUTER_BOUND ( 'NONE', #85610, .T. ) ;
#90665=EDGE_CURVE ( 'NONE', #57717, #13722, #87487, .T. ) ;
#90674=AXIS2_PLACEMENT_3D ( 'NONE', #27574, #73735, #22419 ) ;
#90689=CARTESIAN_POINT ( 'NONE',  ( -1.751198251822016161, 22.56127314141087581, 2.100000000000000089 ) ) ;
#90712=EDGE_CURVE ( 'NONE', #75862, #27531, #56053, .T. ) ;
#90806=DIRECTION ( 'NONE',  ( -1.000000000000000000, 0.000000000000000000, 0.000000000000000000 ) ) ;
#90833=AXIS2_PLACEMENT_3D ( 'NONE', #47872, #32633, #86920 ) ;
#90892=EDGE_CURVE ( 'NONE', #95924, #80254, #59991, .T. ) ;
#90903=CIRCLE ( 'NONE', #3441, 0.2499999999997798983 ) ;
#90932=DIRECTION ( 'NONE',  ( -1.000000000000000000, 0.000000000000000000, 0.000000000000000000 ) ) ;
#90951=AXIS2_PLACEMENT_3D ( 'NONE', #46002, #97775, #5927 ) ;
#90981=VERTEX_POINT ( 'NONE', #12349 ) ;
#91035=LINE ( 'NONE', #36758, #95767 ) ;
#91121=ORIENTED_EDGE ( 'NONE', *, *, #52108, .T. ) ;
#91177=CARTESIAN_POINT ( 'NONE',  ( 8.499999999999989342, 18.74999999999999645, 0.000000000000000000 ) ) ;
#91199=DIRECTION ( 'NONE',  ( 0.000000000000000000, 0.000000000000000000, 1.000000000000000000 ) ) ;
#91211=DIRECTION ( 'NONE',  ( -0.000000000000000000, -0.000000000000000000, -1.000000000000000000 ) ) ;
#91244=ORIENTED_EDGE ( 'NONE', *, *, #17882, .F. ) ;
#91255=DIRECTION ( 'NONE',  ( 0.000000000000000000, -0.000000000000000000, -1.000000000000000000 ) ) ;
#91339=VECTOR ( 'NONE', #28896, 1000.000000000000000 ) ;
#91340=ORIENTED_EDGE ( 'NONE', *, *, #39984, .F. ) ;
#91344=EDGE_CURVE ( 'NONE', #56484, #34878, #7548, .T. ) ;
#91345=ORIENTED_EDGE ( 'NONE', *, *, #33502, .F. ) ;
#91364=DIRECTION ( 'NONE',  ( -1.000000000000000000, 0.000000000000000000, 0.000000000000000000 ) ) ;
#91367=VECTOR ( 'NONE', #4244, 1000.000000000000000 ) ;
#91379=EDGE_LOOP ( 'NONE', ( #26384, #19885, #13026, #31466 ) ) ;
#91404=CARTESIAN_POINT ( 'NONE',  ( -10.34999999999999254, 1.999999999999999112, 0.000000000000000000 ) ) ;
#91406=LINE ( 'NONE', #84798, #68168 ) ;
#91477=ADVANCED_FACE ( 'NONE', ( #90591 ), #89103, .T. ) ;
#91514=ORIENTED_EDGE ( 'NONE', *, *, #86545, .F. ) ;
#91517=VERTEX_POINT ( 'NONE', #74367 ) ;
#91648=VECTOR ( 'NONE', #88425, 1000.000000000000000 ) ;
#91708=DIRECTION ( 'NONE',  ( -1.000000000000000000, 0.000000000000000000, 0.000000000000000000 ) ) ;
#91742=VERTEX_POINT ( 'NONE', #47921 ) ;
#91813=ORIENTED_EDGE ( 'NONE', *, *, #48878, .T. ) ;
#91829=DIRECTION ( 'NONE',  ( 0.000000000000000000, -0.000000000000000000, -1.000000000000000000 ) ) ;
#91833=EDGE_CURVE ( 'NONE', #56809, #82122, #32682, .T. ) ;
#91857=ADVANCED_FACE ( 'NONE', ( #58535 ), #42327, .F. ) ;
#91918=FACE_OUTER_BOUND ( 'NONE', #95034, .T. ) ;
#91924=DIRECTION ( 'NONE',  ( 0.000000000000000000, -0.000000000000000000, -1.000000000000000000 ) ) ;
#91925=VECTOR ( 'NONE', #82504, 1000.000000000000114 ) ;
#91964=VECTOR ( 'NONE', #14169, 1000.000000000000000 ) ;
#91978=VERTEX_POINT ( 'NONE', #52413 ) ;
#91986=CARTESIAN_POINT ( 'NONE',  ( 6.499999999999992895, -1.784922709757266047E-15, -2.500000000000001332 ) ) ;
#92008=DIRECTION ( 'NONE',  ( 0.000000000000000000, 1.000000000000000000, 0.000000000000000000 ) ) ;
#92072=ORIENTED_EDGE ( 'NONE', *, *, #8701, .F. ) ;
#92115=ORIENTED_EDGE ( 'NONE', *, *, #79693, .T. ) ;
#92177=CARTESIAN_POINT ( 'NONE',  ( 2.499999999999995115, 19.99999999999999645, 0.000000000000000000 ) ) ;
#92199=CARTESIAN_POINT ( 'NONE',  ( 10.34999999999999254, 4.999999999999998224, 2.100000000000000089 ) ) ;
#92242=LINE ( 'NONE', #85131, #517 ) ;
#92260=ORIENTED_EDGE ( 'NONE', *, *, #61005, .T. ) ;
#92261=CARTESIAN_POINT ( 'NONE',  ( 2.499999999999994671, 18.99999999999977618, 0.000000000000000000 ) ) ;
#92367=CARTESIAN_POINT ( 'NONE',  ( 4.621320343559255583, 11.49999999999999645, 2.100000000000000089 ) ) ;
#92380=ORIENTED_EDGE ( 'NONE', *, *, #50241, .F. ) ;
#92443=DIRECTION ( 'NONE',  ( -1.000000000000000000, 0.000000000000000000, 0.000000000000000000 ) ) ;
#92454=CARTESIAN_POINT ( 'NONE',  ( 6.499999999999992895, 2.239999999999996660, 2.100000000000000977 ) ) ;
#92501=CARTESIAN_POINT ( 'NONE',  ( 9.299999999999993605, 12.00000000000002309, 0.000000000000000000 ) ) ;
#92521=CARTESIAN_POINT ( 'NONE',  ( 10.34999999999999254, 4.999999999999998224, 2.100000000000000089 ) ) ;
#92532=CARTESIAN_POINT ( 'NONE',  ( 10.34999999999998010, 22.00000000000000000, 2.100000000000000089 ) ) ;
#92541=VECTOR ( 'NONE', #37634, 1000.000000000000000 ) ;
#92636=VECTOR ( 'NONE', #12296, 1000.000000000000000 ) ;
#92639=CARTESIAN_POINT ( 'NONE',  ( -7.662324775236974972, 31.59999999999999787, 2.100000000000000089 ) ) ;
#92657=CARTESIAN_POINT ( 'NONE',  ( 7.662324775236977636, 31.59999999999999787, 2.100000000000000089 ) ) ;
#92678=DIRECTION ( 'NONE',  ( -0.000000000000000000, -0.000000000000000000, -1.000000000000000000 ) ) ;
#92725=LINE ( 'NONE', #75501, #10789 ) ;
#92861=CARTESIAN_POINT ( 'NONE',  ( -6.499999999999992895, -1.267509437117509414E-15, 0.000000000000000000 ) ) ;
#92875=ORIENTED_EDGE ( 'NONE', *, *, #16821, .F. ) ;
#92890=ADVANCED_FACE ( 'NONE', ( #30708 ), #61678, .F. ) ;
#92893=CARTESIAN_POINT ( 'NONE',  ( -6.499999999999992895, 0.9999999999999997780, 1.084202172485504187E-16 ) ) ;
#92949=CARTESIAN_POINT ( 'NONE',  ( -7.749999999999996447, 23.99999999999999289, 2.100000000000000089 ) ) ;
#92963=ADVANCED_FACE ( 'NONE', ( #55056 ), #41325, .T. ) ;
#92982=ORIENTED_EDGE ( 'NONE', *, *, #62794, .F. ) ;
#93014=VECTOR ( 'NONE', #18811, 1000.000000000000000 ) ;
#93114=EDGE_LOOP ( 'NONE', ( #53975, #64405, #41420, #8598 ) ) ;
#93136=CARTESIAN_POINT ( 'NONE',  ( -8.499999999999987566, 18.74999999999999645, 0.000000000000000000 ) ) ;
#93178=VECTOR ( 'NONE', #57061, 1000.000000000000000 ) ;
#93187=CARTESIAN_POINT ( 'NONE',  ( -4.621320343559624177, 12.75000000000004974, 2.100000000000000089 ) ) ;
#93232=VERTEX_POINT ( 'NONE', #12356 ) ;
#93306=VECTOR ( 'NONE', #91829, 1000.000000000000000 ) ;
#93334=ORIENTED_EDGE ( 'NONE', *, *, #48197, .F. ) ;
#93388=CARTESIAN_POINT ( 'NONE',  ( 2.499999999999993783, 4.999999999999997335, 0.000000000000000000 ) ) ;
#93474=CYLINDRICAL_SURFACE ( 'NONE', #35309, 10.80000000000000782 ) ;
#93506=AXIS2_PLACEMENT_3D ( 'NONE', #63866, #24760, #10543 ) ;
#93508=ORIENTED_EDGE ( 'NONE', *, *, #7328, .T. ) ;
#93522=EDGE_CURVE ( 'NONE', #17108, #16636, #9747, .T. ) ;
#93570=CARTESIAN_POINT ( 'NONE',  ( -2.499999999999993339, 19.99999999999999645, 2.100000000000000089 ) ) ;
#93670=CARTESIAN_POINT ( 'NONE',  ( -10.34999999999999254, 4.999999999999999112, 2.100000000000000089 ) ) ;
#93689=DIRECTION ( 'NONE',  ( -0.000000000000000000, -0.000000000000000000, -1.000000000000000000 ) ) ;
#93711=DIRECTION ( 'NONE',  ( 0.000000000000000000, 0.5144957554275265688, -0.8574929257125440962 ) ) ;
#93714=EDGE_LOOP ( 'NONE', ( #55667, #6299, #60946, #7914 ) ) ;
#93784=EDGE_CURVE ( 'NONE', #19391, #93232, #68535, .T. ) ;
#93811=EDGE_CURVE ( 'NONE', #73380, #48269, #13731, .T. ) ;
#93895=EDGE_LOOP ( 'NONE', ( #2443, #58502, #21006, #10996 ) ) ;
#93950=AXIS2_PLACEMENT_3D ( 'NONE', #7165, #8176, #7672 ) ;
#93966=ORIENTED_EDGE ( 'NONE', *, *, #84226, .F. ) ;
#94031=DIRECTION ( 'NONE',  ( 1.000000000000000000, 0.000000000000000000, 0.000000000000000000 ) ) ;
#94051=FACE_OUTER_BOUND ( 'NONE', #60797, .T. ) ;
#94089=FACE_OUTER_BOUND ( 'NONE', #88801, .T. ) ;
#94116=ORIENTED_EDGE ( 'NONE', *, *, #7328, .F. ) ;
#94189=VERTEX_POINT ( 'NONE', #7071 ) ;
#94217=DIRECTION ( 'NONE',  ( -0.000000000000000000, -0.000000000000000000, -1.000000000000000000 ) ) ;
#94270=CARTESIAN_POINT ( 'NONE',  ( -2.499999999999993339, 19.99999999999999645, 0.000000000000000000 ) ) ;
#94376=FACE_OUTER_BOUND ( 'NONE', #13900, .T. ) ;
#94444=ADVANCED_FACE ( 'NONE', ( #97799, #90191 ), #4959, .F. ) ;
#94493=ORIENTED_EDGE ( 'NONE', *, *, #74563, .F. ) ;
#94782=ADVANCED_FACE ( 'NONE', ( #11449 ), #2859, .T. ) ;
#94985=CIRCLE ( 'NONE', #23714, 0.8500000000000017542 ) ;
#95034=EDGE_LOOP ( 'NONE', ( #85310, #89024, #9682, #87858 ) ) ;
#95064=CARTESIAN_POINT ( 'NONE',  ( -2.499999999999993339, 18.99999999999977618, 0.000000000000000000 ) ) ;
#95077=DIRECTION ( 'NONE',  ( -0.000000000000000000, -0.000000000000000000, -1.000000000000000000 ) ) ;
#95094=VECTOR ( 'NONE', #72830, 1000.000000000000000 ) ;
#95098=LINE ( 'NONE', #25583, #33345 ) ;
#95165=AXIS2_PLACEMENT_3D ( 'NONE', #80271, #96995, #43223 ) ;
#95173=AXIS2_PLACEMENT_3D ( 'NONE', #90541, #82428, #12912 ) ;
#95220=ORIENTED_EDGE ( 'NONE', *, *, #86105, .T. ) ;
#95503=CYLINDRICAL_SURFACE ( 'NONE', #89548, 0.2499999999997798983 ) ;
#95521=ADVANCED_FACE ( 'NONE', ( #6968 ), #22175, .T. ) ;
#95583=ADVANCED_FACE ( 'NONE', ( #13568 ), #5964, .F. ) ;
#95601=LINE ( 'NONE', #26089, #93178 ) ;
#95677=CIRCLE ( 'NONE', #9763, 0.2499999999997798983 ) ;
#95690=DIRECTION ( 'NONE',  ( 1.224646799147353207E-16, -1.000000000000000000, 0.000000000000000000 ) ) ;
#95726=EDGE_CURVE ( 'NONE', #2918, #64945, #66276, .T. ) ;
#95733=ORIENTED_EDGE ( 'NONE', *, *, #58390, .F. ) ;
#95767=VECTOR ( 'NONE', #97649, 1000.000000000000000 ) ;
#95801=ORIENTED_EDGE ( 'NONE', *, *, #70981, .F. ) ;
#95868=ORIENTED_EDGE ( 'NONE', *, *, #2958, .F. ) ;
#95924=VERTEX_POINT ( 'NONE', #24056 ) ;
#95930=DIRECTION ( 'NONE',  ( 1.000000000000000000, -7.960204194457801640E-17, 0.000000000000000000 ) ) ;
#95948=ORIENTED_EDGE ( 'NONE', *, *, #73743, .F. ) ;
#95977=ORIENTED_EDGE ( 'NONE', *, *, #58390, .T. ) ;
#96141=DIRECTION ( 'NONE',  ( -0.000000000000000000, -0.000000000000000000, -1.000000000000000000 ) ) ;
#96353=CARTESIAN_POINT ( 'NONE',  ( 9.749999999999985789, 18.74999999999999645, 2.100000000000000089 ) ) ;
#96367=ORIENTED_EDGE ( 'NONE', *, *, #32641, .F. ) ;
#96376=PLANE ( 'NONE',  #47989 ) ;
#96424=DIRECTION ( 'NONE',  ( 0.000000000000000000, 0.000000000000000000, 1.000000000000000000 ) ) ;
#96451=CARTESIAN_POINT ( 'NONE',  ( 2.899999999999999467, 31.80000000000000071, 2.100000000000000089 ) ) ;
#96498=ORIENTED_EDGE ( 'NONE', *, *, #6352, .F. ) ;
#96522=CARTESIAN_POINT ( 'NONE',  ( -3.749999999999999112, 25.69999999999999574, 2.100000000000000089 ) ) ;
#96536=EDGE_CURVE ( 'NONE', #53704, #59029, #98439, .T. ) ;
#96630=EDGE_CURVE ( 'NONE', #31511, #91517, #19344, .T. ) ;
#96656=DIRECTION ( 'NONE',  ( 0.000000000000000000, -1.000000000000000000, 0.000000000000000000 ) ) ;
#96771=EDGE_CURVE ( 'NONE', #57524, #33368, #54298, .T. ) ;
#96824=VECTOR ( 'NONE', #99859, 1000.000000000000000 ) ;
#96836=ADVANCED_FACE ( 'NONE', ( #64928 ), #18223, .T. ) ;
#96837=LINE ( 'NONE', #28828, #10406 ) ;
#96870=DIRECTION ( 'NONE',  ( 1.000000000000000000, 0.000000000000000000, 0.000000000000000000 ) ) ;
#96901=ORIENTED_EDGE ( 'NONE', *, *, #39610, .T. ) ;
#96918=ORIENTED_EDGE ( 'NONE', *, *, #32810, .F. ) ;
#96995=DIRECTION ( 'NONE',  ( -0.000000000000000000, -0.000000000000000000, -1.000000000000000000 ) ) ;
#96999=DIRECTION ( 'NONE',  ( -1.000000000000000000, 0.000000000000000000, 0.000000000000000000 ) ) ;
#97019=ADVANCED_FACE ( 'NONE', ( #58784 ), #34451, .F. ) ;
#97055=CIRCLE ( 'NONE', #53313, 10.80000000000000782 ) ;
#97056=AXIS2_PLACEMENT_3D ( 'NONE', #81374, #5243, #75735 ) ;
#97106=DIRECTION ( 'NONE',  ( -1.000000000000000000, 0.000000000000000000, 0.000000000000000000 ) ) ;
#97197=ORIENTED_EDGE ( 'NONE', *, *, #72628, .F. ) ;
#97206=EDGE_LOOP ( 'NONE', ( #49268, #90137, #98454, #12097 ) ) ;
#97238=ORIENTED_EDGE ( 'NONE', *, *, #40624, .T. ) ;
#97298=AXIS2_PLACEMENT_3D ( 'NONE', #67399, #75480, #91708 ) ;
#97370=CARTESIAN_POINT ( 'NONE',  ( -6.499999999999992895, 2.573529411764704289, 1.544117647058822929 ) ) ;
#97419=DIRECTION ( 'NONE',  ( -1.000000000000000000, 0.000000000000000000, 0.000000000000000000 ) ) ;
#97435=ADVANCED_FACE ( 'NONE', ( #43807 ), #29068, .T. ) ;
#97446=ADVANCED_FACE ( 'NONE', ( #67160 ), #21439, .F. ) ;
#97453=LINE ( 'NONE', #28938, #67879 ) ;
#97500=CARTESIAN_POINT ( 'NONE',  ( -8.376690734369036662, 11.49999999999999645, 0.000000000000000000 ) ) ;
#97542=AXIS2_PLACEMENT_3D ( 'NONE', #26936, #57904, #73121 ) ;
#97569=CARTESIAN_POINT ( 'NONE',  ( -10.34999999999999254, -1.267509437117509414E-15, 0.000000000000000000 ) ) ;
#97589=AXIS2_PLACEMENT_3D ( 'NONE', #55607, #78416, #84535 ) ;
#97649=DIRECTION ( 'NONE',  ( 0.000000000000000000, -1.000000000000000000, 0.000000000000000000 ) ) ;
#97775=DIRECTION ( 'NONE',  ( -0.000000000000000000, -0.000000000000000000, -1.000000000000000000 ) ) ;
#97785=AXIS2_PLACEMENT_3D ( 'NONE', #9451, #338, #16053 ) ;
#97797=CARTESIAN_POINT ( 'NONE',  ( 8.499999999999989342, 18.74999999999999645, 0.000000000000000000 ) ) ;
#97799=FACE_OUTER_BOUND ( 'NONE', #72991, .T. ) ;
#97814=CARTESIAN_POINT ( 'NONE',  ( 2.899999999999999023, 33.29999999999999716, 0.000000000000000000 ) ) ;
#97815=VECTOR ( 'NONE', #68691, 1000.000000000000114 ) ;
#97852=EDGE_CURVE ( 'NONE', #85757, #41954, #16320, .T. ) ;
#97853=VERTEX_POINT ( 'NONE', #96451 ) ;
#97869=ORIENTED_EDGE ( 'NONE', *, *, #97852, .F. ) ;
#97919=CARTESIAN_POINT ( 'NONE',  ( -7.749999999999996447, 23.99999999999999289, 2.100000000000000089 ) ) ;
#97925=CARTESIAN_POINT ( 'NONE',  ( -6.499999999999992895, 0.000000000000000000, 0.000000000000000000 ) ) ;
#98130=CARTESIAN_POINT ( 'NONE',  ( -2.899999999999996803, 31.80000000000000071, 2.100000000000000089 ) ) ;
#98161=CARTESIAN_POINT ( 'NONE',  ( 7.749999999999998224, 25.69999999999999574, 0.000000000000000000 ) ) ;
#98163=VECTOR ( 'NONE', #49609, 1000.000000000000000 ) ;
#98198=ORIENTED_EDGE ( 'NONE', *, *, #84463, .T. ) ;
#98207=VERTEX_POINT ( 'NONE', #44043 ) ;
#98209=EDGE_CURVE ( 'NONE', #27813, #65922, #51663, .T. ) ;
#98361=VECTOR ( 'NONE', #32505, 1000.000000000000000 ) ;
#98366=ORIENTED_EDGE ( 'NONE', *, *, #52630, .F. ) ;
#98373=VERTEX_POINT ( 'NONE', #33814 ) ;
#98437=CARTESIAN_POINT ( 'NONE',  ( -7.749999999999996447, 25.69999999999999574, 2.100000000000000089 ) ) ;
#98439=LINE ( 'NONE', #28434, #46881 ) ;
#98441=AXIS2_PLACEMENT_3D ( 'NONE', #2196, #4187, #88925 ) ;
#98454=ORIENTED_EDGE ( 'NONE', *, *, #22237, .F. ) ;
#98470=EDGE_LOOP ( 'NONE', ( #91340, #563, #29978, #25345 ) ) ;
#98551=LINE ( 'NONE', #12319, #51030 ) ;
#98604=CARTESIAN_POINT ( 'NONE',  ( -8.499999999999987566, 19.99999999999999289, 2.100000000000000089 ) ) ;
#98631=CARTESIAN_POINT ( 'NONE',  ( 8.376690734369038438, 12.50000000000004974, 0.000000000000000000 ) ) ;
#98633=DIRECTION ( 'NONE',  ( -0.000000000000000000, -0.000000000000000000, -1.000000000000000000 ) ) ;
#98635=AXIS2_PLACEMENT_3D ( 'NONE', #57787, #41058, #17210 ) ;
#98799=VECTOR ( 'NONE', #33556, 1000.000000000000000 ) ;
#98805=CIRCLE ( 'NONE', #93950, 1.050000000000000488 ) ;
#98878=DIRECTION ( 'NONE',  ( -0.000000000000000000, -0.000000000000000000, -1.000000000000000000 ) ) ;
#98898=LINE ( 'NONE', #5060, #11962 ) ;
#98936=VERTEX_POINT ( 'NONE', #74735 ) ;
#99197=VERTEX_POINT ( 'NONE', #96353 ) ;
#99207=EDGE_LOOP ( 'NONE', ( #12850, #73252, #73536, #42724 ) ) ;
#99209=ORIENTED_EDGE ( 'NONE', *, *, #70987, .T. ) ;
#99234=DIRECTION ( 'NONE',  ( -1.000000000000000000, -0.000000000000000000, -0.000000000000000000 ) ) ;
#99251=ORIENTED_EDGE ( 'NONE', *, *, #87582, .T. ) ;
#99276=CARTESIAN_POINT ( 'NONE',  ( -10.34999999999999254, 3.299745742347187193E-16, 2.100000000000000977 ) ) ;
#99368=CARTESIAN_POINT ( 'NONE',  ( 4.621320343559262689, 12.74999999999999645, 0.000000000000000000 ) ) ;
#99396=PLANE ( 'NONE',  #88770 ) ;
#99399=CARTESIAN_POINT ( 'NONE',  ( 4.621320343559255583, 11.49999999999999645, 0.000000000000000000 ) ) ;
#99441=DIRECTION ( 'NONE',  ( 1.000000000000000000, 0.000000000000000000, 0.000000000000000000 ) ) ;
#99454=ORIENTED_EDGE ( 'NONE', *, *, #61005, .F. ) ;
#99565=ORIENTED_EDGE ( 'NONE', *, *, #30701, .F. ) ;
#99649=DIRECTION ( 'NONE',  ( -1.000000000000000000, 0.000000000000000000, 0.000000000000000000 ) ) ;
#99857=EDGE_LOOP ( 'NONE', ( #22620, #20233, #23110, #68072 ) ) ;
#99859=DIRECTION ( 'NONE',  ( 1.000000000000000000, 4.986391167143583514E-16, 0.000000000000000000 ) ) ;
#99989=CIRCLE ( 'NONE', #10937, 0.8500000000000017542 ) ;
#100031=ADVANCED_FACE ( 'NONE', ( #40202 ), #34099, .T. ) ;
#100110=DIRECTION ( 'NONE',  ( 0.000000000000000000, -0.000000000000000000, -1.000000000000000000 ) ) ;
#100146=CIRCLE ( 'NONE', #17616, 0.2500000000000011102 ) ;
#100211=ADVANCED_FACE ( 'NONE', ( #62432 ), #8142, .T. ) ;
#100214=DIRECTION ( 'NONE',  ( -0.000000000000000000, -0.000000000000000000, -1.000000000000000000 ) ) ;
#100312=ORIENTED_EDGE ( 'NONE', *, *, #12531, .F. ) ;
#100434=COLOUR_RGB('Deep Blue', 0.66274510, 0.83137255, 0.94901961);
#100435=FILL_AREA_STYLE_COLOUR('',#100434);
#100436=FILL_AREA_STYLE('',(#100435));
#100437=SURFACE_STYLE_FILL_AREA(#100436);
#100438=SURFACE_SIDE_STYLE('',(#100437));
#100439=SURFACE_STYLE_USAGE(.BOTH.,#100438);
#100440=PRESENTATION_STYLE_ASSIGNMENT((#100439));
#100480=STYLED_ITEM('',(#100440),#8170);
#100481=MECHANICAL_DESIGN_GEOMETRIC_PRESENTATION_REPRESENTATION('',(#100480),#27759);
ENDSEC;
END-ISO-10303-21;
